ISO-10303-21;
HEADER;
FILE_DESCRIPTION (('STEP AP214'),
    '1' );
FILE_NAME ('Hex Nut.step',
    '2026-10-09T10:51:02',
    ( '' ),
    ( '' ),
    'SwSTEP 2.0',
    'SolidWorks 2026',
    '' );
FILE_SCHEMA (( 'AUTOMOTIVE_DESIGN' ));
ENDSEC;

DATA;
#17=ORIENTED_EDGE ( 'NONE', *, *, #6536, .F. ) ;
#80=FACE_BOUND ( 'NONE', #4943, .T. ) ;
#98=B_SPLINE_CURVE_WITH_KNOTS ( 'NONE', 3,
 ( #3660, #13798, #8829, #3553, #7001, #21013, #121, #3202 ),
 .UNSPECIFIED., .F., .F.,
 ( 4, 2, 2, 4 ),
 ( 0.005257893453559988640, 0.006567392922673305836, 0.007876892391786622163, 0.01049589133001326002 ),
 .UNSPECIFIED. ) ;
#102=CARTESIAN_POINT ( 'NONE',  ( -0.5772765004791020615, 70.09252763182293222, -80.84070517186570726 ) ) ;
#105=CARTESIAN_POINT ( 'NONE',  ( -9.809641362382285124, 82.00000000000000000, -87.34492244913440118 ) ) ;
#120=EDGE_LOOP ( 'NONE', ( #22099, #16462, #18730 ) ) ;
#121=CARTESIAN_POINT ( 'NONE',  ( -10.95382118728219289, 70.55908004698140701, -92.00507013140023105 ) ) ;
#131=VECTOR ( 'NONE', #1451, 999.9999999999998863 ) ;
#137=B_SPLINE_CURVE_WITH_KNOTS ( 'NONE', 3,
 ( #19717, #16214, #455, #4105, #14828, #14494 ),
 .UNSPECIFIED., .F., .F.,
 ( 4, 2, 4 ),
 ( 2.380730968138597170E-07, 0.002629065763328322300, 0.005257893453559830781 ),
 .UNSPECIFIED. ) ;
#223=DIRECTION ( 'NONE',  ( 0.9232306267972774094, 0.000000000000000000, -0.3842462878721227826 ) ) ;
#228=CARTESIAN_POINT ( 'NONE',  ( -1.163172771417702700, 69.99999999999998579, -89.99248318111824574 ) ) ;
#233=DIRECTION ( 'NONE',  ( -0.9232306267972774094, 0.000000000000000000, 0.3842462878721227826 ) ) ;
#251=VERTEX_POINT ( 'NONE', #22395 ) ;
#255=ORIENTED_EDGE ( 'NONE', *, *, #12322, .T. ) ;
#268=DIRECTION ( 'NONE',  ( 0.9232306267972772984, 0.000000000000000000, -0.3842462878721232822 ) ) ;
#299=CARTESIAN_POINT ( 'NONE',  ( -5.672696058028124710, 81.44153265534504271, -98.91173476717540325 ) ) ;
#300=CARTESIAN_POINT ( 'NONE',  ( -1.163172771417702700, 81.97459999999998104, -89.99248318111824574 ) ) ;
#306=B_SPLINE_CURVE_WITH_KNOTS ( 'NONE', 3,
 ( #21331, #5362, #6982, #1942, #105, #14363 ),
 .UNSPECIFIED., .F., .F.,
 ( 4, 2, 4 ),
 ( 0.009270618776430233909, 0.01189894710419334665, 0.01452727543195645940 ),
 .UNSPECIFIED. ) ;
#383=CARTESIAN_POINT ( 'NONE',  ( -1.163172771417702700, 81.34441321561124028, -89.99248318111824574 ) ) ;
#409=CONICAL_SURFACE ( 'NONE', #3707, 9.000000000000001776, 1.047197551196594301 ) ;
#428=ORIENTED_EDGE ( 'NONE', *, *, #10191, .F. ) ;
#440=VERTEX_POINT ( 'NONE', #6206 ) ;
#455=CARTESIAN_POINT ( 'NONE',  ( 3.457270245634820327, 70.35631045439366460, -98.46779458785445627 ) ) ;
#472=VECTOR ( 'NONE', #7451, 999.9999999999998863 ) ;
#497=DIRECTION ( 'NONE',  ( -5.440186201345738641E-18, -1.000000000000000000, -1.334940939666364181E-17 ) ) ;
#501=ORIENTED_EDGE ( 'NONE', *, *, #10667, .T. ) ;
#505=EDGE_LOOP ( 'NONE', ( #7650, #1698, #13427, #501, #958, #22475 ) ) ;
#514=EDGE_CURVE ( 'NONE', #4756, #20909, #13458, .T. ) ;
#535=CARTESIAN_POINT ( 'NONE',  ( -0.4408429396002319645, 70.00000000000001421, -98.97428162928153483 ) ) ;
#583=CARTESIAN_POINT ( 'NONE',  ( -1.749069042356329984, 81.90747236817705357, -99.14426119037085527 ) ) ;
#648=CARTESIAN_POINT ( 'NONE',  ( -1.163172771417702700, 70.63018678438872655, -89.99248318111824574 ) ) ;
#680=VERTEX_POINT ( 'NONE', #12184 ) ;
#787=ADVANCED_FACE ( 'NONE', ( #15987 ), #20417, .T. ) ;
#794=EDGE_CURVE ( 'NONE', #251, #18403, #137, .T. ) ;
#800=VERTEX_POINT ( 'NONE', #21662 ) ;
#840=CIRCLE ( 'NONE', #8152, 6.000000000000000888 ) ;
#905=ORIENTED_EDGE ( 'NONE', *, *, #14262, .T. ) ;
#928=ORIENTED_EDGE ( 'NONE', *, *, #6703, .F. ) ;
#940=ORIENTED_EDGE ( 'NONE', *, *, #6561, .T. ) ;
#958=ORIENTED_EDGE ( 'NONE', *, *, #16190, .T. ) ;
#1037=CARTESIAN_POINT ( 'NONE',  ( -5.871648968083819753, 81.34441321561124028, -88.03282711297042340 ) ) ;
#1040=DIRECTION ( 'NONE',  ( 0.9232306267972774094, 0.000000000000000000, -0.3842462878721227826 ) ) ;
#1068=VERTEX_POINT ( 'NONE', #1649 ) ;
#1073=FACE_OUTER_BOUND ( 'NONE', #12996, .T. ) ;
#1095=AXIS2_PLACEMENT_3D ( 'NONE', #15139, #6392, #3151 ) ;
#1119=DIRECTION ( 'NONE',  ( -5.440186201345738641E-18, -1.000000000000000000, -1.334940939666364181E-17 ) ) ;
#1144=VECTOR ( 'NONE', #20408, 1000.000000000000000 ) ;
#1168=CARTESIAN_POINT ( 'NONE',  ( 3.346350515192618058, 81.44153265534507113, -81.07323159506104560 ) ) ;
#1198=CYLINDRICAL_SURFACE ( 'NONE', #14793, 5.100000000000000533 ) ;
#1199=AXIS2_PLACEMENT_3D ( 'NONE', #18776, #9937, #15135 ) ;
#1209=DIRECTION ( 'NONE',  ( 0.9232306267972774094, 0.000000000000000000, -0.3842462878721227826 ) ) ;
#1232=DIRECTION ( 'NONE',  ( 0.9232306267972777425, 0.000000000000000000, -0.3842462878721221164 ) ) ;
#1234=CARTESIAN_POINT ( 'NONE',  ( 5.986268468634207807, 81.99999999999998579, -84.52572088931836447 ) ) ;
#1326=DIRECTION ( 'NONE',  ( -0.9232306267972777425, 0.000000000000000000, 0.3842462878721220054 ) ) ;
#1343=CARTESIAN_POINT ( 'NONE',  ( 7.055447609860086011, 81.90747236817705357, -85.92399523110739779 ) ) ;
#1346=EDGE_CURVE ( 'NONE', #680, #1692, #13503, .T. ) ;
#1354=CARTESIAN_POINT ( 'NONE',  ( 5.986268468634207807, 69.99999999999998579, -84.52572088931836447 ) ) ;
#1395=DIRECTION ( 'NONE',  ( 1.000000000000000000, 0.000000000000000000, 0.000000000000000000 ) ) ;
#1451=DIRECTION ( 'NONE',  ( 0.7562662552911951774, 0.5735764363510490460, -0.3147561322209052048 ) ) ;
#1474=( NAMED_UNIT ( * ) SI_UNIT ( $, .STERADIAN. ) SOLID_ANGLE_UNIT ( ) );
#1479=ORIENTED_EDGE ( 'NONE', *, *, #22347, .F. ) ;
#1517=ORIENTED_EDGE ( 'NONE', *, *, #11816, .T. ) ;
#1546=ORIENTED_EDGE ( 'NONE', *, *, #3211, .T. ) ;
#1585=SURFACE_STYLE_FILL_AREA ( #10197 ) ;
#1611=CARTESIAN_POINT ( 'NONE',  ( 8.492591494844877076, 81.64068272718454011, -90.21500375438164099 ) ) ;
#1626=CARTESIAN_POINT ( 'NONE',  ( -0.4408429396002318534, 81.99999999999998579, -98.97428162928156326 ) ) ;
#1649=CARTESIAN_POINT ( 'NONE',  ( -11.46885069223597853, 70.80384757729338219, -91.33151364841882014 ) ) ;
#1665=ADVANCED_FACE ( 'NONE', ( #14150 ), #3943, .T. ) ;
#1671=EDGE_CURVE ( 'NONE', #14389, #20401, #13864, .T. ) ;
#1674=ADVANCED_FACE ( 'NONE', ( #10680 ), #1765, .T. ) ;
#1692=VERTEX_POINT ( 'NONE', #19518 ) ;
#1698=ORIENTED_EDGE ( 'NONE', *, *, #13573, .F. ) ;
#1709=CARTESIAN_POINT ( 'NONE',  ( -1.885502603235176045, 70.00000000000001421, -81.01068473295498507 ) ) ;
#1749=DIRECTION ( 'NONE',  ( 0.9232306267972774094, 0.000000000000000000, -0.3842462878721227826 ) ) ;
#1760=ORIENTED_EDGE ( 'NONE', *, *, #14884, .F. ) ;
#1765=CONICAL_SURFACE ( 'NONE', #4670, 9.000000000000001776, 1.047197551196594301 ) ;
#1793=FACE_OUTER_BOUND ( 'NONE', #9967, .T. ) ;
#1797=ADVANCED_FACE ( 'NONE', ( #11142 ), #18161, .T. ) ;
#1804=ORIENTED_EDGE ( 'NONE', *, *, #3211, .F. ) ;
#1844=ADVANCED_FACE ( 'NONE', ( #1793 ), #9093, .F. ) ;
#1942=CARTESIAN_POINT ( 'NONE',  ( -10.14484841738276089, 81.92452521006620714, -88.15032624680998197 ) ) ;
#2001=ORIENTED_EDGE ( 'NONE', *, *, #7053, .F. ) ;
#2024=CARTESIAN_POINT ( 'NONE',  ( -3.200698602031742723, 70.00000000000000000, -81.18156990192605349 ) ) ;
#2110=DIRECTION ( 'NONE',  ( -5.440186201345738641E-18, -1.000000000000000000, -1.334940939666364181E-17 ) ) ;
#2111=PLANE ( 'NONE',  #9688 ) ;
#2160=CARTESIAN_POINT ( 'NONE',  ( -1.163172771417702700, 69.99999999999998579, -89.99248318111824574 ) ) ;
#2173=CIRCLE ( 'NONE', #20872, 5.999999999999999112 ) ;
#2174=CARTESIAN_POINT ( 'NONE',  ( -3.467698610696717143, 81.64298031427459534, -99.36756502071499142 ) ) ;
#2176=ORIENTED_EDGE ( 'NONE', *, *, #10086, .F. ) ;
#2198=LINE ( 'NONE', #3918, #11033 ) ;
#2235=ORIENTED_EDGE ( 'NONE', *, *, #9722, .T. ) ;
#2238=FACE_OUTER_BOUND ( 'NONE', #7299, .T. ) ;
#2286=EDGE_CURVE ( 'NONE', #21806, #4488, #16115, .T. ) ;
#2296=EDGE_LOOP ( 'NONE', ( #15726, #20627 ) ) ;
#2315=EDGE_CURVE ( 'NONE', #440, #20401, #15092, .T. ) ;
#2318=ORIENTED_EDGE ( 'NONE', *, *, #14884, .T. ) ;
#2359=CARTESIAN_POINT ( 'NONE',  ( -1.163172771417702700, 69.99999999999998579, -89.99248318111824574 ) ) ;
#2369=CARTESIAN_POINT ( 'NONE',  ( -3.467698610696716699, 70.35701968572543308, -99.36756502071496300 ) ) ;
#2416=EDGE_LOOP ( 'NONE', ( #17996, #22055, #8671, #13420, #1804, #7996 ) ) ;
#2417=CARTESIAN_POINT ( 'NONE',  ( 5.448539043597400600, 70.00000000000000000, -83.82247741134344210 ) ) ;
#2425=AXIS2_PLACEMENT_3D ( 'NONE', #20329, #11379, #1040 ) ;
#2427=CARTESIAN_POINT ( 'NONE',  ( -4.067676644731616165, 81.92338897118681018, -81.29421751449218903 ) ) ;
#2526=EDGE_CURVE ( 'NONE', #18327, #800, #14644, .T. ) ;
#2546=CARTESIAN_POINT ( 'NONE',  ( 1.741331101896218758, 81.92338897118678176, -98.69074884774437351 ) ) ;
#2547=DIRECTION ( 'NONE',  ( 0.9232306267972768543, 0.000000000000000000, -0.3842462878721241704 ) ) ;
#2576=DIRECTION ( 'NONE',  ( 0.9916643202943333790, -7.114886815082621371E-18, 0.1288482667915162028 ) ) ;
#2628=DIRECTION ( 'NONE',  ( -0.9232306267972774094, 0.000000000000000000, 0.3842462878721227826 ) ) ;
#2659=CARTESIAN_POINT ( 'NONE',  ( 5.986268468634207807, 81.99999999999998579, -84.52572088931836447 ) ) ;
#2704=ORIENTED_EDGE ( 'NONE', *, *, #15287, .F. ) ;
#2761=VERTEX_POINT ( 'NONE', #6436 ) ;
#2779=CARTESIAN_POINT ( 'NONE',  ( -9.472248412593200939, 69.99999999999998579, -86.53426659026914081 ) ) ;
#2848=CARTESIAN_POINT ( 'NONE',  ( 7.825680009415360239, 70.07756262466202202, -91.81739557479740199 ) ) ;
#2863=EDGE_CURVE ( 'NONE', #3975, #21200, #16504, .T. ) ;
#2910=ORIENTED_EDGE ( 'NONE', *, *, #794, .F. ) ;
#2939=DIRECTION ( 'NONE',  ( -0.7943823600057680068, 1.243025994321579861E-17, -0.6074180324222080429 ) ) ;
#2957=CARTESIAN_POINT ( 'NONE',  ( 9.142505149400571796, 70.80384757729338219, -88.65345271381767134 ) ) ;
#3056=ORIENTED_EDGE ( 'NONE', *, *, #13781, .T. ) ;
#3062=CARTESIAN_POINT ( 'NONE',  ( 7.319796769195226815, 70.14698466122824527, -86.26971152178253988 ) ) ;
#3063=VERTEX_POINT ( 'NONE', #9028 ) ;
#3076=CARTESIAN_POINT ( 'NONE',  ( 7.145902869757795983, 69.99999999999998579, -93.45069977196735067 ) ) ;
#3102=CARTESIAN_POINT ( 'NONE',  ( 0.000000000000000000, 0.000000000000000000, 0.000000000000000000 ) ) ;
#3112=EDGE_CURVE ( 'NONE', #5442, #4756, #8820, .T. ) ;
#3151=DIRECTION ( 'NONE',  ( 0.9232306267972780756, 0.000000000000000000, -0.3842462878721211728 ) ) ;
#3175=FILL_AREA_STYLE_COLOUR ( '', #14775 ) ;
#3202=CARTESIAN_POINT ( 'NONE',  ( -11.46885069223597853, 70.80384757729338219, -91.33151364841882014 ) ) ;
#3211=EDGE_CURVE ( 'NONE', #5755, #8095, #4433, .T. ) ;
#3357=VERTEX_POINT ( 'NONE', #10104 ) ;
#3359=ORIENTED_EDGE ( 'NONE', *, *, #3708, .F. ) ;
#3394=CONICAL_SURFACE ( 'NONE', #7063, 9.000000000000001776, 1.047197551196594301 ) ;
#3430=DIRECTION ( 'NONE',  ( -5.440186201345738641E-18, -1.000000000000000000, -1.334940939666364181E-17 ) ) ;
#3453=EDGE_LOOP ( 'NONE', ( #22641, #8728, #19679, #6787 ) ) ;
#3530=DIRECTION ( 'NONE',  ( -5.440186201345738641E-18, -1.000000000000000000, -1.334940939666364181E-17 ) ) ;
#3552=ORIENTED_EDGE ( 'NONE', *, *, #3872, .T. ) ;
#3553=CARTESIAN_POINT ( 'NONE',  ( -9.381793152695545146, 70.09252763182296064, -94.06097113112909369 ) ) ;
#3563=CARTESIAN_POINT ( 'NONE',  ( -10.95382118728218224, 81.44091995301859299, -92.00507013140021684 ) ) ;
#3654=DIRECTION ( 'NONE',  ( -5.440186201345738641E-18, -1.000000000000000000, -1.334940939666364181E-17 ) ) ;
#3660=CARTESIAN_POINT ( 'NONE',  ( -8.312614011469616315, 69.99999999999998579, -95.45924547291811280 ) ) ;
#3707=AXIS2_PLACEMENT_3D ( 'NONE', #12500, #10648, #16312 ) ;
#3708=EDGE_CURVE ( 'NONE', #4043, #8178, #9457, .T. ) ;
#3725=CIRCLE ( 'NONE', #12165, 9.000000000000001776 ) ;
#3747=PLANE ( 'NONE',  #18331 ) ;
#3775=DIRECTION ( 'NONE',  ( -5.440186201345738641E-18, -1.000000000000000000, -1.334940939666364181E-17 ) ) ;
#3791=EDGE_CURVE ( 'NONE', #19957, #16597, #6318, .T. ) ;
#3825=ORIENTED_EDGE ( 'NONE', *, *, #2315, .T. ) ;
#3872=EDGE_CURVE ( 'NONE', #3975, #8205, #20298, .T. ) ;
#3890=ORIENTED_EDGE ( 'NONE', *, *, #6561, .F. ) ;
#3918=CARTESIAN_POINT ( 'NONE',  ( 4.376210989365964643, 95.03750572909316929, -92.29796090835097289 ) ) ;
#3935=CARTESIAN_POINT ( 'NONE',  ( -7.475646132950445555, 81.99999999999998579, -81.73701953211951832 ) ) ;
#3943=CONICAL_SURFACE ( 'NONE', #16814, 9.000000000000001776, 1.047197551196594301 ) ;
#3975=VERTEX_POINT ( 'NONE', #15596 ) ;
#3983=CARTESIAN_POINT ( 'NONE',  ( 2.830031787867828275, 81.19615242270661781, -80.39798906481894392 ) ) ;
#4009=CARTESIAN_POINT ( 'NONE',  ( -2.322807172541347498, 81.99999999999998579, -81.06750429846923112 ) ) ;
#4027=ORIENTED_EDGE ( 'NONE', *, *, #13075, .F. ) ;
#4029=FACE_BOUND ( 'NONE', #2296, .T. ) ;
#4032=ORIENTED_EDGE ( 'NONE', *, *, #3791, .F. ) ;
#4035=ADVANCED_FACE ( 'NONE', ( #16626 ), #16109, .T. ) ;
#4043=VERTEX_POINT ( 'NONE', #18439 ) ;
#4067=CARTESIAN_POINT ( 'NONE',  ( 2.830031787867828275, 70.80384757729338219, -80.39798906481894392 ) ) ;
#4105=CARTESIAN_POINT ( 'NONE',  ( 1.741331101896219202, 70.07661102881318982, -98.69074884774435930 ) ) ;
#4122=AXIS2_PLACEMENT_3D ( 'NONE', #2160, #3775, #223 ) ;
#4138=ORIENTED_EDGE ( 'NONE', *, *, #21939, .F. ) ;
#4140=CARTESIAN_POINT ( 'NONE',  ( 5.149300590115022835, 81.19615242270661781, -98.24794683011701579 ) ) ;
#4207=CARTESIAN_POINT ( 'NONE',  ( -1.163172771417702700, 70.69320546282760631, -89.99248318111824574 ) ) ;
#4218=CARTESIAN_POINT ( 'NONE',  ( -6.702556532201369599, 81.97459999999998104, -87.68700545388550438 ) ) ;
#4280=CARTESIAN_POINT ( 'NONE',  ( -5.156377330703261208, 81.99999999999998579, -99.58697729741760440 ) ) ;
#4287=ORIENTED_EDGE ( 'NONE', *, *, #12481, .T. ) ;
#4359=CARTESIAN_POINT ( 'NONE',  ( -1.163172771417702478, 95.03750572909316929, -89.99248318111824574 ) ) ;
#4373=CARTESIAN_POINT ( 'NONE',  ( 3.462212668836658125, 70.69320546282760631, -91.91755708335757902 ) ) ;
#4377=EDGE_LOOP ( 'NONE', ( #12923, #8087, #3825, #12795 ) ) ;
#4398=LINE ( 'NONE', #14904, #11420 ) ;
#4433=B_SPLINE_CURVE_WITH_KNOTS ( 'NONE', 3,
 ( #17937, #16562, #13000, #7914, #14839, #19967, #11258, #5622 ),
 .UNSPECIFIED., .F., .F.,
 ( 4, 2, 2, 4 ),
 ( 0.005257893453559862873, 0.006567392922673212161, 0.007876892391786561448, 0.01049589133001325308 ),
 .UNSPECIFIED. ) ;
#4475=VERTEX_POINT ( 'NONE', #7169 ) ;
#4488=VERTEX_POINT ( 'NONE', #12463 ) ;
#4505=ADVANCED_FACE ( 'NONE', ( #21279 ), #5546, .F. ) ;
#4520=DIRECTION ( 'NONE',  ( 0.9232306267972774094, 0.000000000000000000, -0.3842462878721227826 ) ) ;
#4551=APPLICATION_CONTEXT ( 'automotive_design' ) ;
#4567=LINE ( 'NONE', #18590, #15826 ) ;
#4582=EDGE_LOOP ( 'NONE', ( #15004, #4855, #2910 ) ) ;
#4586=CARTESIAN_POINT ( 'NONE',  ( 9.142505149400548703, 81.99999999999998579, -88.65345271381772818 ) ) ;
#4600=DIRECTION ( 'NONE',  ( -5.440186201345739411E-18, -1.000000000000000000, -1.334940939666364181E-17 ) ) ;
#4634=CARTESIAN_POINT ( 'NONE',  ( -1.163172771417702700, 69.99999999999998579, -89.99248318111824574 ) ) ;
#4656=CARTESIAN_POINT ( 'NONE',  ( -1.163172771417702700, 81.99999999999998579, -89.99248318111824574 ) ) ;
#4661=ORIENTED_EDGE ( 'NONE', *, *, #20081, .T. ) ;
#4670=AXIS2_PLACEMENT_3D ( 'NONE', #21347, #17710, #233 ) ;
#4749=CARTESIAN_POINT ( 'NONE',  ( 4.376210989365964643, 81.97459999999998104, -92.29796090835097289 ) ) ;
#4756=VERTEX_POINT ( 'NONE', #18365 ) ;
#4803=CARTESIAN_POINT ( 'NONE',  ( -5.788558211672063969, 70.69320546282760631, -88.06740927887889825 ) ) ;
#4839=ORIENTED_EDGE ( 'NONE', *, *, #15442, .T. ) ;
#4855=ORIENTED_EDGE ( 'NONE', *, *, #20081, .F. ) ;
#4862=CARTESIAN_POINT ( 'NONE',  ( -6.632709584382701529, 81.44153265534507113, -81.62749566292762893 ) ) ;
#4901=( NAMED_UNIT ( * ) PLANE_ANGLE_UNIT ( ) SI_UNIT ( $, .RADIAN. ) );
#4912=DIRECTION ( 'NONE',  ( 0.9232306267972774094, 0.000000000000000000, -0.3842462878721227826 ) ) ;
#4943=EDGE_LOOP ( 'NONE', ( #4138, #10912 ) ) ;
#4954=ORIENTED_EDGE ( 'NONE', *, *, #794, .T. ) ;
#4958=DIRECTION ( 'NONE',  ( -5.440186201345738641E-18, -1.000000000000000000, -1.334940939666364181E-17 ) ) ;
#4993=ADVANCED_FACE ( 'NONE', ( #80, #5344 ), #3747, .F. ) ;
#5001=ORIENTED_EDGE ( 'NONE', *, *, #16263, .F. ) ;
#5078=UNCERTAINTY_MEASURE_WITH_UNIT (LENGTH_MEASURE( 1.000000000000000082E-05 ), #10154, 'distance_accuracy_value', 'NONE');
#5102=EDGE_CURVE ( 'NONE', #4475, #440, #14303, .T. ) ;
#5154=EDGE_CURVE ( 'NONE', #20401, #14389, #2173, .T. ) ;
#5177=ORIENTED_EDGE ( 'NONE', *, *, #1346, .T. ) ;
#5184=DIRECTION ( 'NONE',  ( 5.440186201345738641E-18, 1.000000000000000000, 1.334940939666364181E-17 ) ) ;
#5185=EDGE_CURVE ( 'NONE', #11619, #5755, #10984, .T. ) ;
#5224=CARTESIAN_POINT ( 'NONE',  ( -9.472248412593200939, 69.99999999999998579, -86.53426659026914081 ) ) ;
#5303=CARTESIAN_POINT ( 'NONE',  ( -1.163172771417702700, 81.99999999999998579, -89.99248318111824574 ) ) ;
#5344=FACE_OUTER_BOUND ( 'NONE', #11037, .T. ) ;
#5361=CARTESIAN_POINT ( 'NONE',  ( -5.156377330703347361, 70.80384757729338219, -99.58697729741749072 ) ) ;
#5362=CARTESIAN_POINT ( 'NONE',  ( -11.14411950718743682, 81.44011527025983810, -90.55128027993727358 ) ) ;
#5386=ORIENTED_EDGE ( 'NONE', *, *, #13036, .T. ) ;
#5442=VERTEX_POINT ( 'NONE', #15198 ) ;
#5464=ORIENTED_EDGE ( 'NONE', *, *, #19528, .T. ) ;
#5492=CARTESIAN_POINT ( 'NONE',  ( -1.163172771417702700, 81.99999999999998579, -89.99248318111824574 ) ) ;
#5529=B_SPLINE_CURVE_WITH_KNOTS ( 'NONE', 3,
 ( #5224, #8666, #21308, #5574, #10635, #21195 ),
 .UNSPECIFIED., .F., .F.,
 ( 4, 2, 4 ),
 ( 0.01452727543195646287, 0.01715716534226977355, 0.01978705525258308423 ),
 .UNSPECIFIED. ) ;
#5546=CYLINDRICAL_SURFACE ( 'NONE', #21938, 6.000000000000000888 ) ;
#5566=EDGE_LOOP ( 'NONE', ( #1546, #11711, #10545 ) ) ;
#5569=CARTESIAN_POINT ( 'NONE',  ( -1.749069042356333537, 70.09252763182293222, -99.14426119037081264 ) ) ;
#5574=CARTESIAN_POINT ( 'NONE',  ( -8.125559787506135834, 70.35931727281543147, -83.29857057268348797 ) ) ;
#5578=VERTEX_POINT ( 'NONE', #14495 ) ;
#5622=CARTESIAN_POINT ( 'NONE',  ( 2.830031787867828275, 81.19615242270661781, -80.39798906481894392 ) ) ;
#5649=CARTESIAN_POINT ( 'NONE',  ( -7.798485590386966315, 81.43869406011346257, -82.51270763647201534 ) ) ;
#5653=FACE_OUTER_BOUND ( 'NONE', #4377, .T. ) ;
#5662=CARTESIAN_POINT ( 'NONE',  ( 6.473302864968231596, 70.07547478993376444, -95.06675942850822025 ) ) ;
#5680=DIRECTION ( 'NONE',  ( -0.1288482667915161195, -1.253717443260671070E-17, 0.9916643202943334900 ) ) ;
#5725=CARTESIAN_POINT ( 'NONE',  ( -2.180642712250696835, 81.85301533877169788, -99.20033613248658355 ) ) ;
#5730=PRODUCT_CONTEXT ( 'NONE', #4551, 'mechanical' ) ;
#5755=VERTEX_POINT ( 'NONE', #6631 ) ;
#5766=CARTESIAN_POINT ( 'NONE',  ( 6.808509919968707358, 69.99999999999998579, -94.26135563083261104 ) ) ;
#5789=PRODUCT_DEFINITION_CONTEXT ( 'detailed design', #7783, 'design' ) ;
#5793=CARTESIAN_POINT ( 'NONE',  ( -7.475646132950445555, 81.99999999999998579, -81.73701953211951832 ) ) ;
#5804=ORIENTED_EDGE ( 'NONE', *, *, #21259, .F. ) ;
#5837=CARTESIAN_POINT ( 'NONE',  ( 3.346350515192610064, 70.55846734465492887, -81.07323159506103138 ) ) ;
#5884=AXIS2_PLACEMENT_3D ( 'NONE', #21336, #3654, #14245 ) ;
#5892=DIRECTION ( 'NONE',  ( -0.9232306267972774094, -1.069144893909151832E-19, 0.3842462878721230046 ) ) ;
#5935=DIRECTION ( 'NONE',  ( -5.440186201345738641E-18, -1.000000000000000000, -1.334940939666364181E-17 ) ) ;
#5938=AXIS2_PLACEMENT_3D ( 'NONE', #22250, #22356, #6541 ) ;
#5973=ORIENTED_EDGE ( 'NONE', *, *, #5185, .T. ) ;
#6071=ORIENTED_EDGE ( 'NONE', *, *, #15423, .F. ) ;
#6092=DIRECTION ( 'NONE',  ( -0.7562662552911934011, -0.5735764363510515995, 0.3147561322209046497 ) ) ;
#6165=ORIENTED_EDGE ( 'NONE', *, *, #11816, .F. ) ;
#6206=CARTESIAN_POINT ( 'NONE',  ( 3.545303425248413465, 70.63018678438872655, -91.95213924926606808 ) ) ;
#6273=CARTESIAN_POINT ( 'NONE',  ( -1.163172771417702700, 70.63018678438872655, -89.99248318111824574 ) ) ;
#6292=AXIS2_PLACEMENT_3D ( 'NONE', #3102, #12069, #1395 ) ;
#6318=B_SPLINE_CURVE_WITH_KNOTS ( 'NONE', 3,
 ( #6350, #9897, #22166, #16918, #8285, #10016 ),
 .UNSPECIFIED., .F., .F.,
 ( 4, 2, 4 ),
 ( 0.009270618776430242583, 0.01189894710419334839, 0.01452727543195645593 ),
 .UNSPECIFIED. ) ;
#6332=PLANE ( 'NONE',  #17467 ) ;
#6343=AXIS2_PLACEMENT_3D ( 'NONE', #10609, #12884, #9415 ) ;
#6344=AXIS2_PLACEMENT_3D ( 'NONE', #5303, #16136, #15912 ) ;
#6350=CARTESIAN_POINT ( 'NONE',  ( 5.149300590115022835, 81.19615242270661781, -98.24794683011701579 ) ) ;
#6387=FACE_OUTER_BOUND ( 'NONE', #3453, .T. ) ;
#6392=DIRECTION ( 'NONE',  ( 5.440186201345738641E-18, 1.000000000000000000, 1.334940939666364181E-17 ) ) ;
#6436=CARTESIAN_POINT ( 'NONE',  ( 7.145902869757795983, 69.99999999999998579, -93.45069977196735067 ) ) ;
#6446=CARTESIAN_POINT ( 'NONE',  ( 4.917494328089510702, 81.92338897118681018, -83.12797620812510502 ) ) ;
#6536=EDGE_CURVE ( 'NONE', #16597, #5442, #18025, .T. ) ;
#6541=DIRECTION ( 'NONE',  ( 0.9232306267972768543, 0.000000000000000000, -0.3842462878721241704 ) ) ;
#6561=EDGE_CURVE ( 'NONE', #1692, #4043, #2198, .T. ) ;
#6563=VECTOR ( 'NONE', #10020, 1000.000000000000114 ) ;
#6568=EDGE_CURVE ( 'NONE', #4488, #440, #14755, .T. ) ;
#6572=LINE ( 'NONE', #17260, #16869 ) ;
#6631=CARTESIAN_POINT ( 'NONE',  ( -2.322807172541347498, 81.99999999999998579, -81.06750429846923112 ) ) ;
#6643=CARTESIAN_POINT ( 'NONE',  ( -8.312614011469616315, 69.99999999999998579, -95.45924547291811280 ) ) ;
#6703=EDGE_CURVE ( 'NONE', #680, #8178, #4567, .T. ) ;
#6712=ORIENTED_EDGE ( 'NONE', *, *, #21939, .T. ) ;
#6721=CARTESIAN_POINT ( 'NONE',  ( 8.627475644446743530, 81.44091995301864984, -87.97989623083630306 ) ) ;
#6731=EDGE_LOOP ( 'NONE', ( #15712, #7448, #14192, #15125 ) ) ;
#6732=CIRCLE ( 'NONE', #8560, 9.000000000000001776 ) ;
#6734=CARTESIAN_POINT ( 'NONE',  ( -4.067676644731632152, 70.07661102881314719, -81.29421751449218903 ) ) ;
#6752=CARTESIAN_POINT ( 'NONE',  ( 1.141353067861252457, 70.35701968572534781, -80.61740134152158532 ) ) ;
#6758=B_SPLINE_CURVE_WITH_KNOTS ( 'NONE', 3,
 ( #8316, #4862, #9309, #2427, #16355, #4009 ),
 .UNSPECIFIED., .F., .F.,
 ( 4, 2, 4 ),
 ( 2.380730968575512647E-07, 0.002629065763328360464, 0.005257893453559862873 ),
 .UNSPECIFIED. ) ;
#6768=CARTESIAN_POINT ( 'NONE',  ( 7.483496276596866004, 81.99999999999998579, -92.63956227386769626 ) ) ;
#6787=ORIENTED_EDGE ( 'NONE', *, *, #5102, .F. ) ;
#6869=EDGE_CURVE ( 'NONE', #4488, #21806, #9609, .T. ) ;
#6896=EDGE_LOOP ( 'NONE', ( #6712, #15947, #20143, #3890 ) ) ;
#6982=CARTESIAN_POINT ( 'NONE',  ( -10.81153106956454479, 81.64473548815914228, -89.75216824834804186 ) ) ;
#7001=CARTESIAN_POINT ( 'NONE',  ( -9.646142312030677957, 70.14698466122825948, -93.71525484045396581 ) ) ;
#7010=ADVANCED_FACE ( 'NONE', ( #9838 ), #15120, .T. ) ;
#7013=CARTESIAN_POINT ( 'NONE',  ( -8.580473483290075976, 81.99999999999994316, -95.10893838946510925 ) ) ;
#7017=CIRCLE ( 'NONE', #12528, 9.000000000000001776 ) ;
#7043=CARTESIAN_POINT ( 'NONE',  ( 7.145902869757795983, 81.99999999999998579, -93.45069977196735067 ) ) ;
#7053=EDGE_CURVE ( 'NONE', #5578, #18403, #3725, .T. ) ;
#7063=AXIS2_PLACEMENT_3D ( 'NONE', #14927, #18790, #20153 ) ;
#7099=CARTESIAN_POINT ( 'NONE',  ( 1.989200010245318895, 70.55908004698136438, -80.50723945831674655 ) ) ;
#7127=B_SPLINE_CURVE_WITH_KNOTS ( 'NONE', 3,
 ( #10000, #1168, #8161, #6446, #20429, #2659 ),
 .UNSPECIFIED., .F., .F.,
 ( 4, 2, 4 ),
 ( 2.380730968275997826E-07, 0.002629065763328383015, 0.005257893453559938333 ),
 .UNSPECIFIED. ) ;
#7147=ORIENTED_EDGE ( 'NONE', *, *, #13781, .F. ) ;
#7169=CARTESIAN_POINT ( 'NONE',  ( -5.871648968083819753, 70.63018678438872655, -88.03282711297042340 ) ) ;
#7204=PRODUCT_DEFINITION_SHAPE ( 'NONE', 'NONE',  #13264 ) ;
#7299=EDGE_LOOP ( 'NONE', ( #255, #11948, #3552, #13856, #1479, #17890 ) ) ;
#7323=ORIENTED_EDGE ( 'NONE', *, *, #514, .T. ) ;
#7335=DIRECTION ( 'NONE',  ( 0.9232306267972774094, 0.000000000000000000, -0.3842462878721227826 ) ) ;
#7367=CARTESIAN_POINT ( 'NONE',  ( -1.163172771417702700, 81.99999999999998579, -89.99248318111824574 ) ) ;
#7378=DIRECTION ( 'NONE',  ( -5.440186201345738641E-18, -1.000000000000000000, -1.334940939666364181E-17 ) ) ;
#7391=( GEOMETRIC_REPRESENTATION_CONTEXT ( 3 ) GLOBAL_UNCERTAINTY_ASSIGNED_CONTEXT ( ( #5078 ) ) GLOBAL_UNIT_ASSIGNED_CONTEXT ( ( #10154, #18759, #15454 ) ) REPRESENTATION_CONTEXT ( 'NONE', 'WORKASPACE' ) );
#7448=ORIENTED_EDGE ( 'NONE', *, *, #10894, .T. ) ;
#7451=DIRECTION ( 'NONE',  ( -0.7562662552911951774, 0.5735764363510490460, 0.3147561322209052603 ) ) ;
#7493=DIRECTION ( 'NONE',  ( -5.440186201345738641E-18, -1.000000000000000000, -1.334940939666364181E-17 ) ) ;
#7514=CARTESIAN_POINT ( 'NONE',  ( 5.474031775163560098, 70.55988472974013348, -97.46771346163548344 ) ) ;
#7527=DIRECTION ( 'NONE',  ( -5.440186201345738641E-18, -1.000000000000000000, -1.334940939666364181E-17 ) ) ;
#7638=DIRECTION ( 'NONE',  ( 0.9232306267972776315, 0.000000000000000000, -0.3842462878721224495 ) ) ;
#7650=ORIENTED_EDGE ( 'NONE', *, *, #13505, .F. ) ;
#7653=AXIS2_PLACEMENT_3D ( 'NONE', #383, #7378, #13043 ) ;
#7681=B_SPLINE_CURVE_WITH_KNOTS ( 'NONE', 3,
 ( #21591, #9432, #14416, #14637, #5649, #16473 ),
 .UNSPECIFIED., .F., .F.,
 ( 4, 2, 4 ),
 ( 0.01452727543195645940, 0.01715716534226981171, 0.01978705525258316056 ),
 .UNSPECIFIED. ) ;
#7750=AXIS2_PLACEMENT_3D ( 'NONE', #19933, #22191, #1326 ) ;
#7783=APPLICATION_CONTEXT ( 'automotive_design' ) ;
#7888=CARTESIAN_POINT ( 'NONE',  ( -1.163172771417702700, 69.99999999999998579, -89.99248318111824574 ) ) ;
#7914=CARTESIAN_POINT ( 'NONE',  ( -0.5772765004791022836, 81.90747236817706778, -80.84070517186573568 ) ) ;
#7963=B_SPLINE_CURVE_WITH_KNOTS ( 'NONE', 3,
 ( #12166, #1709, #17999, #102, #12399, #6752, #7099, #4067 ),
 .UNSPECIFIED., .F., .F.,
 ( 4, 2, 2, 4 ),
 ( 0.005257893453559862873, 0.006567392922673209558, 0.007876892391786556244, 0.01049589133001325482 ),
 .UNSPECIFIED. ) ;
#7972=FACE_OUTER_BOUND ( 'NONE', #9979, .T. ) ;
#7991=ORIENTED_EDGE ( 'NONE', *, *, #19593, .F. ) ;
#7996=ORIENTED_EDGE ( 'NONE', *, *, #18627, .F. ) ;
#8053=ORIENTED_EDGE ( 'NONE', *, *, #2526, .F. ) ;
#8068=CARTESIAN_POINT ( 'NONE',  ( 5.149300590115015730, 81.99999999999998579, -98.24794683011701579 ) ) ;
#8072=EDGE_CURVE ( 'NONE', #21806, #8178, #12516, .T. ) ;
#8086=EDGE_CURVE ( 'NONE', #12626, #5578, #22030, .T. ) ;
#8087=ORIENTED_EDGE ( 'NONE', *, *, #5102, .T. ) ;
#8095=VERTEX_POINT ( 'NONE', #3983 ) ;
#8098=AXIS2_PLACEMENT_3D ( 'NONE', #7367, #5184, #21375 ) ;
#8102=LINE ( 'NONE', #5793, #10023 ) ;
#8135=ORIENTED_EDGE ( 'NONE', *, *, #3872, .F. ) ;
#8142=CARTESIAN_POINT ( 'NONE',  ( -8.312614011469616315, 81.99999999999998579, -95.45924547291811280 ) ) ;
#8152=AXIS2_PLACEMENT_3D ( 'NONE', #22570, #10664, #14130 ) ;
#8161=CARTESIAN_POINT ( 'NONE',  ( 3.866440703273599677, 81.64368954560637803, -81.75340644824424885 ) ) ;
#8162=DIRECTION ( 'NONE',  ( -5.440186201345738641E-18, -1.000000000000000000, -1.334940939666364181E-17 ) ) ;
#8178=VERTEX_POINT ( 'NONE', #4218 ) ;
#8205=VERTEX_POINT ( 'NONE', #11244 ) ;
#8226=CARTESIAN_POINT ( 'NONE',  ( 6.523188911928189171, 81.98100004360546222, -85.22790637956201465 ) ) ;
#8285=CARTESIAN_POINT ( 'NONE',  ( 6.808509919968707358, 82.00000000000000000, -94.26135563083259683 ) ) ;
#8316=CARTESIAN_POINT ( 'NONE',  ( -7.475646132950418021, 81.19615242270661781, -81.73701953211944726 ) ) ;
#8335=DIRECTION ( 'NONE',  ( 5.440186201345738641E-18, 1.000000000000000000, 1.334940939666364181E-17 ) ) ;
#8355=CARTESIAN_POINT ( 'NONE',  ( -6.192786246109101889, 70.35631045439366460, -98.23155991399221421 ) ) ;
#8398=DIRECTION ( 'NONE',  ( 0.9232306267972774094, 0.000000000000000000, -0.3842462878721227826 ) ) ;
#8457=AXIS2_PLACEMENT_3D ( 'NONE', #10078, #2939, #22541 ) ;
#8559=ADVANCED_FACE ( 'NONE', ( #19817 ), #12116, .F. ) ;
#8560=AXIS2_PLACEMENT_3D ( 'NONE', #9071, #10704, #1749 ) ;
#8666=CARTESIAN_POINT ( 'NONE',  ( -9.134655005754131807, 69.99999999999998579, -85.72312909216951482 ) ) ;
#8671=ORIENTED_EDGE ( 'NONE', *, *, #14196, .T. ) ;
#8675=SURFACE_STYLE_USAGE ( .BOTH. , #20751 ) ;
#8684=DIRECTION ( 'NONE',  ( -0.6074180324222083760, -7.300068142772954271E-18, 0.7943823600057675627 ) ) ;
#8710=EDGE_LOOP ( 'NONE', ( #14140, #2318, #13734 ) ) ;
#8728=ORIENTED_EDGE ( 'NONE', *, *, #6869, .F. ) ;
#8820=B_SPLINE_CURVE_WITH_KNOTS ( 'NONE', 3,
 ( #17367, #1626, #18051, #583, #5725, #2174, #18374, #11365 ),
 .UNSPECIFIED., .F., .F.,
 ( 4, 2, 2, 4 ),
 ( 0.005257893453559830781, 0.006567392922673205222, 0.007876892391786580530, 0.01049589133001331900 ),
 .UNSPECIFIED. ) ;
#8829=CARTESIAN_POINT ( 'NONE',  ( -8.849534454763650970, 70.01899995639456620, -94.75705998267451946 ) ) ;
#8986=EDGE_LOOP ( 'NONE', ( #21163, #21866, #10225 ) ) ;
#9028=CARTESIAN_POINT ( 'NONE',  ( 5.986268468634207807, 81.99999999999998579, -84.52572088931836447 ) ) ;
#9039=ORIENTED_EDGE ( 'NONE', *, *, #8086, .F. ) ;
#9071=CARTESIAN_POINT ( 'NONE',  ( -1.163172771417702700, 69.99999999999998579, -89.99248318111824574 ) ) ;
#9078=CARTESIAN_POINT ( 'NONE',  ( 4.306364041547309895, 81.44153265534502850, -98.35747069930887676 ) ) ;
#9088=DIRECTION ( 'NONE',  ( -5.440186201345738641E-18, -1.000000000000000000, -1.334940939666364181E-17 ) ) ;
#9090=EDGE_LOOP ( 'NONE', ( #4027, #11947, #2704 ) ) ;
#9093=CONICAL_SURFACE ( 'NONE', #10207, 6.000000000000000888, 0.9599310885968777018 ) ;
#9221=DIRECTION ( 'NONE',  ( 0.9232306267972777425, 0.000000000000000000, -0.3842462878721220054 ) ) ;
#9223=CARTESIAN_POINT ( 'NONE',  ( 7.145902869757795983, 69.99999999999998579, -93.45069977196735067 ) ) ;
#9235=ADVANCED_FACE ( 'NONE', ( #17801 ), #409, .T. ) ;
#9245=CARTESIAN_POINT ( 'NONE',  ( -7.243839870924983160, 81.92338897118676755, -96.85699015411138646 ) ) ;
#9309=CARTESIAN_POINT ( 'NONE',  ( -5.783615788470215513, 81.64368954560637803, -81.51717177438210626 ) ) ;
#9361=B_SPLINE_CURVE_WITH_KNOTS ( 'NONE', 3,
 ( #17983, #7514, #12697, #5662, #5766, #9223 ),
 .UNSPECIFIED., .F., .F.,
 ( 4, 2, 4 ),
 ( 0.009270618776430230440, 0.01189894710419334319, 0.01452727543195645593 ),
 .UNSPECIFIED. ) ;
#9415=DIRECTION ( 'NONE',  ( -0.9232306267972774094, 0.000000000000000000, 0.3842462878721227826 ) ) ;
#9432=CARTESIAN_POINT ( 'NONE',  ( -9.134655005754124701, 81.99999999999998579, -85.72312909216948640 ) ) ;
#9457=CIRCLE ( 'NONE', #13156, 6.000000000000000888 ) ;
#9501=ADVANCED_FACE ( 'NONE', ( #18873 ), #11426, .F. ) ;
#9556=CARTESIAN_POINT ( 'NONE',  ( -9.472248412593200939, 69.99999999999998579, -86.53426659026914081 ) ) ;
#9598=DIRECTION ( 'NONE',  ( 5.440186201345738641E-18, 1.000000000000000000, 1.334940939666364181E-17 ) ) ;
#9609=CIRCLE ( 'NONE', #14399, 5.100000000000004974 ) ;
#9668=CARTESIAN_POINT ( 'NONE',  ( -7.475646132950418021, 81.19615242270661781, -81.73701953211944726 ) ) ;
#9681=CLOSED_SHELL ( 'NONE', ( #22548, #9501, #8559, #17231, #18577, #1797, #14213, #10501, #21083, #15961, #13553, #9788, #4993, #7010, #4035, #14998, #10477, #1665, #20031, #18726, #14338, #1674, #9235, #12341, #787, #16527, #1844, #4505 ) ) ;
#9688=AXIS2_PLACEMENT_3D ( 'NONE', #3935, #5892, #16272 ) ;
#9708=FACE_OUTER_BOUND ( 'NONE', #11187, .T. ) ;
#9722=EDGE_CURVE ( 'NONE', #11619, #20328, #7681, .T. ) ;
#9741=CARTESIAN_POINT ( 'NONE',  ( -1.163172771417702700, 81.99999999999998579, -89.99248318111824574 ) ) ;
#9761=CARTESIAN_POINT ( 'NONE',  ( -11.46885069223597853, 81.99999999999998579, -91.33151364841880593 ) ) ;
#9788=ADVANCED_FACE ( 'NONE', ( #4029, #19880 ), #11058, .T. ) ;
#9806=DIRECTION ( 'NONE',  ( -5.440186201345738641E-18, -1.000000000000000000, -1.334940939666364181E-17 ) ) ;
#9838=FACE_OUTER_BOUND ( 'NONE', #8986, .T. ) ;
#9859=CARTESIAN_POINT ( 'NONE',  ( 8.819665691964026166, 70.56130593988652322, -89.42914081817022520 ) ) ;
#9897=CARTESIAN_POINT ( 'NONE',  ( 5.474031775163563651, 81.44011527025983810, -97.46771346163548344 ) ) ;
#9937=DIRECTION ( 'NONE',  ( -5.440186201345738641E-18, -1.000000000000000000, -1.334940939666364181E-17 ) ) ;
#9967=EDGE_LOOP ( 'NONE', ( #12533, #12213, #14330, #3359 ) ) ;
#9979=EDGE_LOOP ( 'NONE', ( #2001, #7147, #13460 ) ) ;
#9989=STYLED_ITEM ( 'NONE', ( #15725 ), #17010 ) ;
#10000=CARTESIAN_POINT ( 'NONE',  ( 2.830031787867828275, 81.19615242270661781, -80.39798906481894392 ) ) ;
#10016=CARTESIAN_POINT ( 'NONE',  ( 7.145902869757795983, 81.99999999999998579, -93.45069977196735067 ) ) ;
#10020=DIRECTION ( 'NONE',  ( 0.7562662552911934011, -0.5735764363510514885, -0.3147561322209044832 ) ) ;
#10023=VECTOR ( 'NONE', #21749, 1000.000000000000000 ) ;
#10078=CARTESIAN_POINT ( 'NONE',  ( -11.46885069223597853, 81.99999999999998579, -91.33151364841880593 ) ) ;
#10086=EDGE_CURVE ( 'NONE', #3357, #3975, #18907, .T. ) ;
#10104=CARTESIAN_POINT ( 'NONE',  ( 2.830031787867828275, 70.80384757729338219, -80.39798906481894392 ) ) ;
#10145=FACE_OUTER_BOUND ( 'NONE', #20183, .T. ) ;
#10154=( LENGTH_UNIT ( ) NAMED_UNIT ( * ) SI_UNIT ( .MILLI., .METRE. ) );
#10191=EDGE_CURVE ( 'NONE', #800, #1068, #15051, .T. ) ;
#10197=FILL_AREA_STYLE ('',( #3175 ) ) ;
#10207=AXIS2_PLACEMENT_3D ( 'NONE', #300, #17665, #21421 ) ;
#10225=ORIENTED_EDGE ( 'NONE', *, *, #21259, .T. ) ;
#10252=ORIENTED_EDGE ( 'NONE', *, *, #13573, .T. ) ;
#10416=CARTESIAN_POINT ( 'NONE',  ( -5.783615788470239494, 70.35631045439365039, -81.51717177438210626 ) ) ;
#10434=EDGE_CURVE ( 'NONE', #4475, #14389, #21913, .T. ) ;
#10477=ADVANCED_FACE ( 'NONE', ( #18391 ), #11219, .T. ) ;
#10501=ADVANCED_FACE ( 'NONE', ( #11846 ), #6332, .F. ) ;
#10512=EDGE_CURVE ( 'NONE', #8095, #3063, #7127, .T. ) ;
#10545=ORIENTED_EDGE ( 'NONE', *, *, #12481, .F. ) ;
#10609=CARTESIAN_POINT ( 'NONE',  ( -1.163172771417702700, 69.99999999999998579, -89.99248318111824574 ) ) ;
#10635=CARTESIAN_POINT ( 'NONE',  ( -7.798485590386990296, 70.56130593988649480, -82.51270763647208639 ) ) ;
#10648=DIRECTION ( 'NONE',  ( 5.440186201345738641E-18, 1.000000000000000000, 1.334940939666364181E-17 ) ) ;
#10664=DIRECTION ( 'NONE',  ( -5.440186201345738641E-18, -1.000000000000000000, -1.334940939666364181E-17 ) ) ;
#10667=EDGE_CURVE ( 'NONE', #16597, #19220, #14261, .T. ) ;
#10680=FACE_OUTER_BOUND ( 'NONE', #21848, .T. ) ;
#10704=DIRECTION ( 'NONE',  ( -5.440186201345738641E-18, -1.000000000000000000, -1.334940939666364181E-17 ) ) ;
#10756=CARTESIAN_POINT ( 'NONE',  ( -5.156377330703347361, 81.19615242270661781, -99.58697729741749072 ) ) ;
#10820=CONICAL_SURFACE ( 'NONE', #17431, 9.000000000000001776, 1.047197551196594301 ) ;
#10882=ORIENTED_EDGE ( 'NONE', *, *, #3708, .T. ) ;
#10894=EDGE_CURVE ( 'NONE', #4488, #4043, #12009, .T. ) ;
#10912=ORIENTED_EDGE ( 'NONE', *, *, #1346, .F. ) ;
#10931=VERTEX_POINT ( 'NONE', #16851 ) ;
#10947=AXIS2_PLACEMENT_3D ( 'NONE', #16438, #5680, #20965 ) ;
#10984=CIRCLE ( 'NONE', #1095, 9.000000000000003553 ) ;
#11033=VECTOR ( 'NONE', #7493, 1000.000000000000000 ) ;
#11037=EDGE_LOOP ( 'NONE', ( #5804, #11246, #905, #5386, #5973, #4287 ) ) ;
#11039=CIRCLE ( 'NONE', #5884, 9.000000000000001776 ) ;
#11058=PLANE ( 'NONE',  #13414 ) ;
#11061=AXIS2_PLACEMENT_3D ( 'NONE', #2359, #13063, #21618 ) ;
#11076=CONICAL_SURFACE ( 'NONE', #22406, 5.010000000000001563, 0.9599310885968744822 ) ;
#11085=ORIENTED_EDGE ( 'NONE', *, *, #21292, .F. ) ;
#11142=FACE_OUTER_BOUND ( 'NONE', #2416, .T. ) ;
#11168=DIRECTION ( 'NONE',  ( 5.440186201345738641E-18, 1.000000000000000000, 1.334940939666364181E-17 ) ) ;
#11177=AXIS2_PLACEMENT_3D ( 'NONE', #19149, #14004, #8684 ) ;
#11187=EDGE_LOOP ( 'NONE', ( #10252, #4954, #4839, #17601, #16613, #11912 ) ) ;
#11219=CONICAL_SURFACE ( 'NONE', #2425, 9.000000000000001776, 1.047197551196594301 ) ;
#11244=CARTESIAN_POINT ( 'NONE',  ( 9.142505149400571796, 70.80384757729338219, -88.65345271381767134 ) ) ;
#11246=ORIENTED_EDGE ( 'NONE', *, *, #6536, .T. ) ;
#11258=CARTESIAN_POINT ( 'NONE',  ( 1.989200010245318451, 81.44091995301859299, -80.50723945831674655 ) ) ;
#11337=DIRECTION ( 'NONE',  ( -5.440186201345738641E-18, -1.000000000000000000, -1.334940939666364181E-17 ) ) ;
#11365=CARTESIAN_POINT ( 'NONE',  ( -5.156377330703347361, 81.19615242270661781, -99.58697729741749072 ) ) ;
#11379=DIRECTION ( 'NONE',  ( -5.440186201345738641E-18, -1.000000000000000000, -1.334940939666364181E-17 ) ) ;
#11420=VECTOR ( 'NONE', #7527, 1000.000000000000000 ) ;
#11426=CONICAL_SURFACE ( 'NONE', #7750, 6.000000000000000888, 0.9599310885968777018 ) ;
#11450=CARTESIAN_POINT ( 'NONE',  ( 2.830031787867825166, 81.99999999999998579, -80.39798906481894392 ) ) ;
#11505=CARTESIAN_POINT ( 'NONE',  ( -5.156377330703261208, 81.99999999999998579, -99.58697729741760440 ) ) ;
#11576=B_SPLINE_CURVE_WITH_KNOTS ( 'NONE', 3,
 ( #5361, #17115, #8355, #15399, #22346, #6643 ),
 .UNSPECIFIED., .F., .F.,
 ( 4, 2, 4 ),
 ( 2.380730969743839749E-07, 0.002629065763328481461, 0.005257893453559988640 ),
 .UNSPECIFIED. ) ;
#11581=EDGE_CURVE ( 'NONE', #19957, #5442, #18711, .T. ) ;
#11614=DIRECTION ( 'NONE',  ( -0.9232306267972774094, -1.069144893909151832E-19, 0.3842462878721230046 ) ) ;
#11619=VERTEX_POINT ( 'NONE', #18841 ) ;
#11684=ORIENTED_EDGE ( 'NONE', *, *, #2286, .F. ) ;
#11685=CARTESIAN_POINT ( 'NONE',  ( 6.254127940454620393, 70.00000000000000000, -84.87602797277139643 ) ) ;
#11711=ORIENTED_EDGE ( 'NONE', *, *, #10512, .T. ) ;
#11816=EDGE_CURVE ( 'NONE', #5578, #1068, #98, .T. ) ;
#11846=FACE_OUTER_BOUND ( 'NONE', #505, .T. ) ;
#11854=CIRCLE ( 'NONE', #6344, 9.000000000000001776 ) ;
#11885=VECTOR ( 'NONE', #13381, 1000.000000000000000 ) ;
#11912=ORIENTED_EDGE ( 'NONE', *, *, #11581, .F. ) ;
#11937=ORIENTED_EDGE ( 'NONE', *, *, #19528, .F. ) ;
#11947=ORIENTED_EDGE ( 'NONE', *, *, #22117, .F. ) ;
#11948=ORIENTED_EDGE ( 'NONE', *, *, #10086, .T. ) ;
#11956=CARTESIAN_POINT ( 'NONE',  ( 9.142505149400571796, 81.19615242270661781, -88.65345271381767134 ) ) ;
#11975=CARTESIAN_POINT ( 'NONE',  ( -9.381793152695534488, 81.90747236817703936, -94.06097113112909369 ) ) ;
#12009=LINE ( 'NONE', #4749, #131 ) ;
#12069=DIRECTION ( 'NONE',  ( 0.000000000000000000, 0.000000000000000000, 1.000000000000000000 ) ) ;
#12077=EDGE_CURVE ( 'NONE', #2761, #8205, #15732, .T. ) ;
#12116=CONICAL_SURFACE ( 'NONE', #18000, 5.010000000000001563, 0.9599310885968744822 ) ;
#12133=CARTESIAN_POINT ( 'NONE',  ( 8.627475644446743530, 70.55908004698135016, -87.97989623083630306 ) ) ;
#12165=AXIS2_PLACEMENT_3D ( 'NONE', #7888, #16755, #16526 ) ;
#12166=CARTESIAN_POINT ( 'NONE',  ( -2.322807172541347498, 69.99999999999998579, -81.06750429846923112 ) ) ;
#12184=CARTESIAN_POINT ( 'NONE',  ( -6.702556532201366046, 81.99999999999998579, -87.68700545388549017 ) ) ;
#12213=ORIENTED_EDGE ( 'NONE', *, *, #6869, .T. ) ;
#12232=AXIS2_PLACEMENT_3D ( 'NONE', #4656, #8335, #22111 ) ;
#12322=EDGE_CURVE ( 'NONE', #8095, #3357, #16648, .T. ) ;
#12341=ADVANCED_FACE ( 'NONE', ( #22098 ), #3394, .T. ) ;
#12399=CARTESIAN_POINT ( 'NONE',  ( -0.1457028305847437588, 70.14698466122824527, -80.78463022974995056 ) ) ;
#12463=CARTESIAN_POINT ( 'NONE',  ( 3.545303425248414353, 81.34441321561124028, -91.95213924926606808 ) ) ;
#12481=EDGE_CURVE ( 'NONE', #5755, #3063, #11854, .T. ) ;
#12500=CARTESIAN_POINT ( 'NONE',  ( -1.163172771417702700, 69.99999999999998579, -89.99248318111824574 ) ) ;
#12510=DIRECTION ( 'NONE',  ( -5.440186201345738641E-18, -1.000000000000000000, -1.334940939666364181E-17 ) ) ;
#12516=LINE ( 'NONE', #16329, #472 ) ;
#12528=AXIS2_PLACEMENT_3D ( 'NONE', #13827, #4958, #1209 ) ;
#12533=ORIENTED_EDGE ( 'NONE', *, *, #10894, .F. ) ;
#12575=CONICAL_SURFACE ( 'NONE', #13672, 9.000000000000001776, 1.047197551196594301 ) ;
#12583=EDGE_LOOP ( 'NONE', ( #5464, #18386, #20227, #12764 ) ) ;
#12592=VECTOR ( 'NONE', #1119, 1000.000000000000000 ) ;
#12602=CARTESIAN_POINT ( 'NONE',  ( -8.312614011469616315, 81.99999999999998579, -95.45924547291811280 ) ) ;
#12626=VERTEX_POINT ( 'NONE', #9556 ) ;
#12697=CARTESIAN_POINT ( 'NONE',  ( 5.806620212786449464, 70.35526451184087193, -96.66860143004628014 ) ) ;
#12712=ORIENTED_EDGE ( 'NONE', *, *, #21292, .T. ) ;
#12718=DIRECTION ( 'NONE',  ( -5.440186201345738641E-18, -1.000000000000000000, -1.334940939666364181E-17 ) ) ;
#12763=SHAPE_DEFINITION_REPRESENTATION ( #7204, #15770 ) ;
#12764=ORIENTED_EDGE ( 'NONE', *, *, #2315, .F. ) ;
#12795=ORIENTED_EDGE ( 'NONE', *, *, #5154, .T. ) ;
#12820=CARTESIAN_POINT ( 'NONE',  ( -0.003538370294055813436, 69.99999999999998579, -98.91746206376724615 ) ) ;
#12867=CARTESIAN_POINT ( 'NONE',  ( 4.917494328089510702, 70.07661102881314719, -83.12797620812510502 ) ) ;
#12884=DIRECTION ( 'NONE',  ( 5.440186201345738641E-18, 1.000000000000000000, 1.334940939666364181E-17 ) ) ;
#12901=CARTESIAN_POINT ( 'NONE',  ( -10.14484841738276089, 70.07547478993376444, -88.15032624680998197 ) ) ;
#12916=AXIS2_PLACEMENT_3D ( 'NONE', #4280, #14782, #2576 ) ;
#12923=ORIENTED_EDGE ( 'NONE', *, *, #10434, .F. ) ;
#12991=ORIENTED_EDGE ( 'NONE', *, *, #22117, .T. ) ;
#12996=EDGE_LOOP ( 'NONE', ( #11684, #13661, #11937, #15230 ) ) ;
#13000=CARTESIAN_POINT ( 'NONE',  ( -1.446236478174511397, 81.98100004360546222, -80.95361029988728774 ) ) ;
#13004=UNCERTAINTY_MEASURE_WITH_UNIT (LENGTH_MEASURE( 1.000000000000000082E-05 ), #17328, 'distance_accuracy_value', 'NONE');
#13036=EDGE_CURVE ( 'NONE', #18327, #11619, #22095, .T. ) ;
#13038=AXIS2_PLACEMENT_3D ( 'NONE', #15623, #20991, #14361 ) ;
#13042=ORIENTED_EDGE ( 'NONE', *, *, #18627, .T. ) ;
#13043=DIRECTION ( 'NONE',  ( -0.9232306267972776315, 0.000000000000000000, 0.3842462878721224495 ) ) ;
#13063=DIRECTION ( 'NONE',  ( -5.440186201345738641E-18, -1.000000000000000000, -1.334940939666364181E-17 ) ) ;
#13065=CARTESIAN_POINT ( 'NONE',  ( -1.163172771417702700, 81.99999999999998579, -89.99248318111824574 ) ) ;
#13075=EDGE_CURVE ( 'NONE', #12626, #10931, #5529, .T. ) ;
#13084=DIRECTION ( 'NONE',  ( 0.9232306267972774094, 0.000000000000000000, -0.3842462878721227826 ) ) ;
#13156=AXIS2_PLACEMENT_3D ( 'NONE', #14759, #497, #21711 ) ;
#13264=PRODUCT_DEFINITION ( 'UNKNOWN', '', #19809, #5789 ) ;
#13381=DIRECTION ( 'NONE',  ( -5.440186201345738641E-18, -1.000000000000000000, -1.334940939666364181E-17 ) ) ;
#13413=CARTESIAN_POINT ( 'NONE',  ( 6.254127940454616841, 81.99999999999998579, -84.87602797277141065 ) ) ;
#13414=AXIS2_PLACEMENT_3D ( 'NONE', #16915, #4600, #16803 ) ;
#13420=ORIENTED_EDGE ( 'NONE', *, *, #12322, .F. ) ;
#13427=ORIENTED_EDGE ( 'NONE', *, *, #3791, .T. ) ;
#13458=LINE ( 'NONE', #11505, #19668 ) ;
#13460=ORIENTED_EDGE ( 'NONE', *, *, #15442, .F. ) ;
#13486=AXIS2_PLACEMENT_3D ( 'NONE', #228, #20776, #2628 ) ;
#13503=CIRCLE ( 'NONE', #17918, 6.000000000000004441 ) ;
#13505=EDGE_CURVE ( 'NONE', #251, #2761, #9361, .T. ) ;
#13541=CARTESIAN_POINT ( 'NONE',  ( 8.492591494844878852, 70.35931727281543147, -90.21500375438166941 ) ) ;
#13553=ADVANCED_FACE ( 'NONE', ( #21608 ), #2111, .T. ) ;
#13573=EDGE_CURVE ( 'NONE', #19957, #251, #17053, .T. ) ;
#13654=MECHANICAL_DESIGN_GEOMETRIC_PRESENTATION_REPRESENTATION('',(#9989),#16982);
#13661=ORIENTED_EDGE ( 'NONE', *, *, #17372, .T. ) ;
#13672=AXIS2_PLACEMENT_3D ( 'NONE', #17569, #12510, #19498 ) ;
#13734=ORIENTED_EDGE ( 'NONE', *, *, #13036, .F. ) ;
#13743=CARTESIAN_POINT ( 'NONE',  ( 9.142505149400571796, 81.19615242270661781, -88.65345271381767134 ) ) ;
#13757=CARTESIAN_POINT ( 'NONE',  ( -2.322807172541347498, 69.99999999999998579, -81.06750429846923112 ) ) ;
#13781=EDGE_CURVE ( 'NONE', #20909, #5578, #11576, .T. ) ;
#13798=CARTESIAN_POINT ( 'NONE',  ( -8.580473483290074199, 70.00000000000001421, -95.10893838946512346 ) ) ;
#13827=CARTESIAN_POINT ( 'NONE',  ( -1.163172771417702700, 81.99999999999998579, -89.99248318111824574 ) ) ;
#13856=ORIENTED_EDGE ( 'NONE', *, *, #16190, .F. ) ;
#13864=CIRCLE ( 'NONE', #21543, 5.999999999999999112 ) ;
#13875=ORIENTED_EDGE ( 'NONE', *, *, #16263, .T. ) ;
#13984=CARTESIAN_POINT ( 'NONE',  ( 4.376210989365967308, 69.99999999999998579, -92.29796090835098710 ) ) ;
#14004=DIRECTION ( 'NONE',  ( 0.7943823600057676737, -1.243025994321580632E-17, 0.6074180324222084870 ) ) ;
#14033=B_SPLINE_CURVE_WITH_KNOTS ( 'NONE', 3,
 ( #12820, #535, #14454, #5569, #21516, #2369, #19794, #19584 ),
 .UNSPECIFIED., .F., .F.,
 ( 4, 2, 2, 4 ),
 ( 0.005257893453559830781, 0.006567392922673201752, 0.007876892391786571856, 0.01049589133001331553 ),
 .UNSPECIFIED. ) ;
#14042=CARTESIAN_POINT ( 'NONE',  ( -9.646142312030676180, 81.85301533877171209, -93.71525484045396581 ) ) ;
#14130=DIRECTION ( 'NONE',  ( 0.9232306267972777425, 0.000000000000000000, -0.3842462878721220054 ) ) ;
#14140=ORIENTED_EDGE ( 'NONE', *, *, #2526, .T. ) ;
#14150=FACE_OUTER_BOUND ( 'NONE', #120, .T. ) ;
#14192=ORIENTED_EDGE ( 'NONE', *, *, #14900, .F. ) ;
#14196=EDGE_CURVE ( 'NONE', #21200, #3357, #7963, .T. ) ;
#14213=ADVANCED_FACE ( 'NONE', ( #2238 ), #15736, .T. ) ;
#14245=DIRECTION ( 'NONE',  ( 0.9232306267972774094, 0.000000000000000000, -0.3842462878721227826 ) ) ;
#14261=B_SPLINE_CURVE_WITH_KNOTS ( 'NONE', 3,
 ( #19049, #6768, #15749, #1611, #20665, #11956 ),
 .UNSPECIFIED., .F., .F.,
 ( 4, 2, 4 ),
 ( 0.01452727543195645593, 0.01715716534226980478, 0.01978705525258315362 ),
 .UNSPECIFIED. ) ;
#14262=EDGE_CURVE ( 'NONE', #5442, #18327, #17062, .T. ) ;
#14303=CIRCLE ( 'NONE', #16866, 5.100000000000000533 ) ;
#14330=ORIENTED_EDGE ( 'NONE', *, *, #8072, .T. ) ;
#14338=ADVANCED_FACE ( 'NONE', ( #7972 ), #10820, .T. ) ;
#14361=DIRECTION ( 'NONE',  ( 0.9232306267972774094, 0.000000000000000000, -0.3842462878721226160 ) ) ;
#14363=CARTESIAN_POINT ( 'NONE',  ( -9.472248412593195610, 81.99999999999998579, -86.53426659026914081 ) ) ;
#14389=VERTEX_POINT ( 'NONE', #18444 ) ;
#14399=AXIS2_PLACEMENT_3D ( 'NONE', #19263, #3530, #15617 ) ;
#14416=CARTESIAN_POINT ( 'NONE',  ( -8.792471272935635795, 81.92243737533797798, -84.90096239309919213 ) ) ;
#14454=CARTESIAN_POINT ( 'NONE',  ( -0.8801090646609086576, 70.01899995639456620, -99.03135606234927479 ) ) ;
#14463=DIRECTION ( 'NONE',  ( 0.9232306267972772984, 1.069144893909150629E-19, -0.3842462878721229491 ) ) ;
#14480=CONICAL_SURFACE ( 'NONE', #21050, 9.000000000000001776, 1.047197551196594301 ) ;
#14494=CARTESIAN_POINT ( 'NONE',  ( -0.003538370294055813436, 69.99999999999998579, -98.91746206376724615 ) ) ;
#14495=CARTESIAN_POINT ( 'NONE',  ( -8.312614011469616315, 69.99999999999998579, -95.45924547291811280 ) ) ;
#14568=B_SPLINE_CURVE_WITH_KNOTS ( 'NONE', 3,
 ( #22445, #17662, #10416, #6734, #2024, #13757 ),
 .UNSPECIFIED., .F., .F.,
 ( 4, 2, 4 ),
 ( 2.380730968223736687E-07, 0.002629065763328342683, 0.005257893453559862873 ),
 .UNSPECIFIED. ) ;
#14633=CARTESIAN_POINT ( 'NONE',  ( -11.14411950718743682, 70.55988472974013348, -90.55128027993727358 ) ) ;
#14637=CARTESIAN_POINT ( 'NONE',  ( -8.125559787506114517, 81.64068272718454011, -83.29857057268343112 ) ) ;
#14644=B_SPLINE_CURVE_WITH_KNOTS ( 'NONE', 3,
 ( #17250, #7013, #19300, #11975, #14042, #21027, #3563, #21355 ),
 .UNSPECIFIED., .F., .F.,
 ( 4, 2, 2, 4 ),
 ( 0.005257893453559989508, 0.006567392922673304101, 0.007876892391786620429, 0.01049589133001324961 ),
 .UNSPECIFIED. ) ;
#14668=DIRECTION ( 'NONE',  ( -5.440186201345738641E-18, -1.000000000000000000, -1.334940939666364181E-17 ) ) ;
#14751=DIRECTION ( 'NONE',  ( -5.440186201345738641E-18, -1.000000000000000000, -1.334940939666364181E-17 ) ) ;
#14755=LINE ( 'NONE', #16469, #1144 ) ;
#14759=CARTESIAN_POINT ( 'NONE',  ( -1.163172771417702700, 81.97459999999998104, -89.99248318111824574 ) ) ;
#14775=COLOUR_RGB ( '', 0.08235294, 0.09019608, 0.10196078) ;
#14782=DIRECTION ( 'NONE',  ( 0.1288482667915162305, 1.253717443260671224E-17, -0.9916643202943334900 ) ) ;
#14793=AXIS2_PLACEMENT_3D ( 'NONE', #15103, #12718, #16300 ) ;
#14828=CARTESIAN_POINT ( 'NONE',  ( 0.8743530591963382115, 70.00000000000002842, -98.80339646031046641 ) ) ;
#14839=CARTESIAN_POINT ( 'NONE',  ( -0.1457028305847436478, 81.85301533877176894, -80.78463022974997898 ) ) ;
#14868=CARTESIAN_POINT ( 'NONE',  ( -10.81153106956454479, 70.35526451184087193, -89.75216824834804186 ) ) ;
#14884=EDGE_CURVE ( 'NONE', #800, #11619, #306, .T. ) ;
#14900=EDGE_CURVE ( 'NONE', #8178, #4043, #840, .T. ) ;
#14902=PRODUCT ( 'Hex Nut', 'Hex Nut', '', ( #5730 ) ) ;
#14904=CARTESIAN_POINT ( 'NONE',  ( 9.142505149400548703, 81.99999999999998579, -88.65345271381772818 ) ) ;
#14927=CARTESIAN_POINT ( 'NONE',  ( -1.163172771417702700, 69.99999999999998579, -89.99248318111824574 ) ) ;
#14968=CARTESIAN_POINT ( 'NONE',  ( -1.163172771417702700, 81.99999999999998579, -89.99248318111824574 ) ) ;
#14998=ADVANCED_FACE ( 'NONE', ( #21216 ), #12575, .T. ) ;
#15004=ORIENTED_EDGE ( 'NONE', *, *, #13505, .T. ) ;
#15017=DIRECTION ( 'NONE',  ( 0.9232306267972765212, 0.000000000000000000, -0.3842462878721248920 ) ) ;
#15051=LINE ( 'NONE', #9761, #16008 ) ;
#15075=ORIENTED_EDGE ( 'NONE', *, *, #11581, .T. ) ;
#15092=LINE ( 'NONE', #4373, #6563 ) ;
#15103=CARTESIAN_POINT ( 'NONE',  ( -1.163172771417702700, 81.99999999999998579, -89.99248318111824574 ) ) ;
#15120=CONICAL_SURFACE ( 'NONE', #21672, 9.000000000000001776, 1.047197551196594301 ) ;
#15125=ORIENTED_EDGE ( 'NONE', *, *, #8072, .F. ) ;
#15130=ORIENTED_EDGE ( 'NONE', *, *, #2863, .F. ) ;
#15135=DIRECTION ( 'NONE',  ( 0.9232306267972776315, 0.000000000000000000, -0.3842462878721224495 ) ) ;
#15139=CARTESIAN_POINT ( 'NONE',  ( -1.163172771417702700, 81.99999999999998579, -89.99248318111824574 ) ) ;
#15198=CARTESIAN_POINT ( 'NONE',  ( -0.003538370294055813436, 81.99999999999998579, -98.91746206376724615 ) ) ;
#15230=ORIENTED_EDGE ( 'NONE', *, *, #6568, .F. ) ;
#15257=CARTESIAN_POINT ( 'NONE',  ( 7.319796769195229480, 81.85301533877174052, -86.26971152178252567 ) ) ;
#15283=CARTESIAN_POINT ( 'NONE',  ( 7.483496276596866892, 69.99999999999998579, -92.63956227386769626 ) ) ;
#15287=EDGE_CURVE ( 'NONE', #10931, #21200, #14568, .T. ) ;
#15341=SHAPE_REPRESENTATION_RELATIONSHIP ( 'NONE' , 'NONE' ,  #15770, #15403 ) ;
#15354=CYLINDRICAL_SURFACE ( 'NONE', #1199, 5.100000000000000533 ) ;
#15374=CARTESIAN_POINT ( 'NONE',  ( 6.523188911928190059, 70.01899995639452356, -85.22790637956202886 ) ) ;
#15399=CARTESIAN_POINT ( 'NONE',  ( -7.243839870924989377, 70.07661102881318982, -96.85699015411138646 ) ) ;
#15403=ADVANCED_BREP_SHAPE_REPRESENTATION ( '', ( #17010, #6292 ), #7391 ) ;
#15423=EDGE_CURVE ( 'NONE', #4756, #18327, #17047, .T. ) ;
#15442=EDGE_CURVE ( 'NONE', #18403, #20909, #14033, .T. ) ;
#15451=CARTESIAN_POINT ( 'NONE',  ( -2.322807172541347498, 69.99999999999998579, -81.06750429846923112 ) ) ;
#15454=( NAMED_UNIT ( * ) SI_UNIT ( $, .STERADIAN. ) SOLID_ANGLE_UNIT ( ) );
#15456=B_SPLINE_CURVE_WITH_KNOTS ( 'NONE', 3,
 ( #1234, #13413, #8226, #1343, #15257, #22208, #6721, #13743 ),
 .UNSPECIFIED., .F., .F.,
 ( 4, 2, 2, 4 ),
 ( 0.005257893453559938333, 0.006567392922673252059, 0.007876892391786564918, 0.01049589133001322533 ),
 .UNSPECIFIED. ) ;
#15596=CARTESIAN_POINT ( 'NONE',  ( 5.986268468634207807, 69.99999999999998579, -84.52572088931836447 ) ) ;
#15617=DIRECTION ( 'NONE',  ( -0.9232306267972765212, 0.000000000000000000, 0.3842462878721248920 ) ) ;
#15623=CARTESIAN_POINT ( 'NONE',  ( -1.163172771417702700, 81.99999999999998579, -89.99248318111824574 ) ) ;
#15712=ORIENTED_EDGE ( 'NONE', *, *, #2286, .T. ) ;
#15725=PRESENTATION_STYLE_ASSIGNMENT (( #8675 ) ) ;
#15726=ORIENTED_EDGE ( 'NONE', *, *, #5154, .F. ) ;
#15732=B_SPLINE_CURVE_WITH_KNOTS ( 'NONE', 3,
 ( #3076, #15283, #2848, #13541, #9859, #2957 ),
 .UNSPECIFIED., .F., .F.,
 ( 4, 2, 4 ),
 ( 0.01452727543195645593, 0.01715716534226980824, 0.01978705525258316056 ),
 .UNSPECIFIED. ) ;
#15736=PLANE ( 'NONE',  #11177 ) ;
#15749=CARTESIAN_POINT ( 'NONE',  ( 7.825680009415360239, 81.92243737533797798, -91.81739557479740199 ) ) ;
#15770=SHAPE_REPRESENTATION ( 'Hex Nut', ( #6292 ), #7391 ) ;
#15826=VECTOR ( 'NONE', #16882, 1000.000000000000000 ) ;
#15912=DIRECTION ( 'NONE',  ( 0.9232306267972774094, 0.000000000000000000, -0.3842462878721227826 ) ) ;
#15947=ORIENTED_EDGE ( 'NONE', *, *, #6703, .T. ) ;
#15956=EDGE_LOOP ( 'NONE', ( #22582, #12712, #16479, #7991, #17042, #1760 ) ) ;
#15961=ADVANCED_FACE ( 'NONE', ( #17186 ), #17427, .T. ) ;
#15987=FACE_OUTER_BOUND ( 'NONE', #18795, .T. ) ;
#15994=DIRECTION ( 'NONE',  ( -5.440186201345738641E-18, -1.000000000000000000, -1.334940939666364181E-17 ) ) ;
#16008=VECTOR ( 'NONE', #18694, 1000.000000000000000 ) ;
#16109=CONICAL_SURFACE ( 'NONE', #22647, 9.000000000000001776, 1.047197551196594301 ) ;
#16115=CIRCLE ( 'NONE', #7653, 5.100000000000000533 ) ;
#16136=DIRECTION ( 'NONE',  ( 5.440186201345738641E-18, 1.000000000000000000, 1.334940939666364181E-17 ) ) ;
#16190=EDGE_CURVE ( 'NONE', #19220, #8205, #4398, .T. ) ;
#16214=CARTESIAN_POINT ( 'NONE',  ( 4.306364041547310784, 70.55846734465492887, -98.35747069930887676 ) ) ;
#16263=EDGE_CURVE ( 'NONE', #2761, #3975, #19468, .T. ) ;
#16272=DIRECTION ( 'NONE',  ( -5.440186201345738641E-18, -1.000000000000000000, -1.334940939666364181E-17 ) ) ;
#16300=DIRECTION ( 'NONE',  ( 0.9232306267972776315, 0.000000000000000000, -0.3842462878721224495 ) ) ;
#16312=DIRECTION ( 'NONE',  ( -0.9232306267972774094, 0.000000000000000000, 0.3842462878721227826 ) ) ;
#16329=CARTESIAN_POINT ( 'NONE',  ( -6.702556532201369599, 81.97459999999998104, -87.68700545388550438 ) ) ;
#16355=CARTESIAN_POINT ( 'NONE',  ( -3.200698602031736950, 81.99999999999998579, -81.18156990192605349 ) ) ;
#16438=CARTESIAN_POINT ( 'NONE',  ( 2.830031787867825166, 81.99999999999998579, -80.39798906481894392 ) ) ;
#16443=CARTESIAN_POINT ( 'NONE',  ( 5.986268468634207807, 69.99999999999998579, -84.52572088931836447 ) ) ;
#16462=ORIENTED_EDGE ( 'NONE', *, *, #15423, .T. ) ;
#16469=CARTESIAN_POINT ( 'NONE',  ( 3.545303425248413465, 81.99999999999998579, -91.95213924926606808 ) ) ;
#16473=CARTESIAN_POINT ( 'NONE',  ( -7.475646132950418021, 81.19615242270661781, -81.73701953211944726 ) ) ;
#16479=ORIENTED_EDGE ( 'NONE', *, *, #13075, .T. ) ;
#16504=CIRCLE ( 'NONE', #20861, 9.000000000000001776 ) ;
#16526=DIRECTION ( 'NONE',  ( 0.9232306267972774094, 0.000000000000000000, -0.3842462878721227826 ) ) ;
#16527=ADVANCED_FACE ( 'NONE', ( #5653 ), #11076, .F. ) ;
#16562=CARTESIAN_POINT ( 'NONE',  ( -1.885502603235176489, 82.00000000000000000, -81.01068473295497085 ) ) ;
#16586=CARTESIAN_POINT ( 'NONE',  ( 3.457270245634818995, 81.64368954560634961, -98.46779458785447048 ) ) ;
#16597=VERTEX_POINT ( 'NONE', #7043 ) ;
#16613=ORIENTED_EDGE ( 'NONE', *, *, #3112, .F. ) ;
#16626=FACE_OUTER_BOUND ( 'NONE', #5566, .T. ) ;
#16648=LINE ( 'NONE', #11450, #12592 ) ;
#16745=DIRECTION ( 'NONE',  ( 5.440186201345738641E-18, 1.000000000000000000, 1.334940939666364181E-17 ) ) ;
#16755=DIRECTION ( 'NONE',  ( -5.440186201345738641E-18, -1.000000000000000000, -1.334940939666364181E-17 ) ) ;
#16803=DIRECTION ( 'NONE',  ( 0.9232306267972772984, 1.069144893909150629E-19, -0.3842462878721229491 ) ) ;
#16814=AXIS2_PLACEMENT_3D ( 'NONE', #5492, #21128, #7335 ) ;
#16824=EDGE_LOOP ( 'NONE', ( #928, #5177, #940, #10882 ) ) ;
#16848=CARTESIAN_POINT ( 'NONE',  ( -1.163172771417702700, 69.99999999999998579, -89.99248318111824574 ) ) ;
#16851=CARTESIAN_POINT ( 'NONE',  ( -7.475646132950445555, 70.80384757729335377, -81.73701953211951832 ) ) ;
#16866=AXIS2_PLACEMENT_3D ( 'NONE', #6273, #21525, #7638 ) ;
#16869=VECTOR ( 'NONE', #18964, 1000.000000000000000 ) ;
#16882=DIRECTION ( 'NONE',  ( -5.440186201345738641E-18, -1.000000000000000000, -1.334940939666364181E-17 ) ) ;
#16908=FACE_OUTER_BOUND ( 'NONE', #6896, .T. ) ;
#16915=CARTESIAN_POINT ( 'NONE',  ( -17.78132405376864966, 69.99999999999998579, -83.07604999942009272 ) ) ;
#16918=CARTESIAN_POINT ( 'NONE',  ( 6.473302864968229819, 81.92452521006620714, -95.06675942850819183 ) ) ;
#16982=( GEOMETRIC_REPRESENTATION_CONTEXT ( 3 ) GLOBAL_UNCERTAINTY_ASSIGNED_CONTEXT ( ( #13004 ) ) GLOBAL_UNIT_ASSIGNED_CONTEXT ( ( #17328, #4901, #1474 ) ) REPRESENTATION_CONTEXT ( 'NONE', 'WORKASPACE' ) );
#17010=MANIFOLD_SOLID_BREP ( 'Stock-MAS-425-1', #9681 ) ;
#17042=ORIENTED_EDGE ( 'NONE', *, *, #9722, .F. ) ;
#17047=B_SPLINE_CURVE_WITH_KNOTS ( 'NONE', 3,
 ( #10756, #299, #21303, #9245, #18120, #12602 ),
 .UNSPECIFIED., .F., .F.,
 ( 4, 2, 4 ),
 ( 2.380730969749054296E-07, 0.002629065763328481894, 0.005257893453559989508 ),
 .UNSPECIFIED. ) ;
#17053=LINE ( 'NONE', #8068, #11885 ) ;
#17062=CIRCLE ( 'NONE', #13038, 9.000000000000005329 ) ;
#17115=CARTESIAN_POINT ( 'NONE',  ( -5.672696058028122934, 70.55846734465492887, -98.91173476717540325 ) ) ;
#17186=FACE_OUTER_BOUND ( 'NONE', #17475, .T. ) ;
#17231=ADVANCED_FACE ( 'NONE', ( #1073 ), #1198, .F. ) ;
#17250=CARTESIAN_POINT ( 'NONE',  ( -8.312614011469616315, 81.99999999999998579, -95.45924547291811280 ) ) ;
#17260=CARTESIAN_POINT ( 'NONE',  ( -5.871648968083818865, 81.99999999999998579, -88.03282711297042340 ) ) ;
#17328=( LENGTH_UNIT ( ) NAMED_UNIT ( * ) SI_UNIT ( .MILLI., .METRE. ) );
#17367=CARTESIAN_POINT ( 'NONE',  ( -0.003538370294055813436, 81.99999999999998579, -98.91746206376724615 ) ) ;
#17372=EDGE_CURVE ( 'NONE', #21806, #4475, #6572, .T. ) ;
#17427=PLANE ( 'NONE',  #8457 ) ;
#17431=AXIS2_PLACEMENT_3D ( 'NONE', #4634, #9598, #22080 ) ;
#17467=AXIS2_PLACEMENT_3D ( 'NONE', #4586, #11614, #18604 ) ;
#17475=EDGE_LOOP ( 'NONE', ( #7323, #3056, #1517, #428, #8053, #6071 ) ) ;
#17550=DIRECTION ( 'NONE',  ( -5.440186201345739411E-18, -1.000000000000000000, -1.334940939666364181E-17 ) ) ;
#17569=CARTESIAN_POINT ( 'NONE',  ( -1.163172771417702700, 81.99999999999998579, -89.99248318111824574 ) ) ;
#17601=ORIENTED_EDGE ( 'NONE', *, *, #514, .F. ) ;
#17662=CARTESIAN_POINT ( 'NONE',  ( -6.632709584382732615, 70.55846734465490044, -81.62749566292762893 ) ) ;
#17665=DIRECTION ( 'NONE',  ( 5.440186201345738641E-18, 1.000000000000000000, 1.334940939666364181E-17 ) ) ;
#17710=DIRECTION ( 'NONE',  ( 5.440186201345738641E-18, 1.000000000000000000, 1.334940939666364181E-17 ) ) ;
#17736=ORIENTED_EDGE ( 'NONE', *, *, #8086, .T. ) ;
#17801=FACE_OUTER_BOUND ( 'NONE', #9090, .T. ) ;
#17877=CARTESIAN_POINT ( 'NONE',  ( -1.163172771417702478, 95.03750572909316929, -89.99248318111824574 ) ) ;
#17890=ORIENTED_EDGE ( 'NONE', *, *, #10512, .F. ) ;
#17918=AXIS2_PLACEMENT_3D ( 'NONE', #14968, #11168, #2547 ) ;
#17937=CARTESIAN_POINT ( 'NONE',  ( -2.322807172541347498, 81.99999999999998579, -81.06750429846923112 ) ) ;
#17983=CARTESIAN_POINT ( 'NONE',  ( 5.149300590115022835, 70.80384757729338219, -98.24794683011701579 ) ) ;
#17996=ORIENTED_EDGE ( 'NONE', *, *, #19593, .T. ) ;
#17999=CARTESIAN_POINT ( 'NONE',  ( -1.446236478174512063, 70.01899995639453778, -80.95361029988728774 ) ) ;
#18000=AXIS2_PLACEMENT_3D ( 'NONE', #4207, #5935, #20391 ) ;
#18025=CIRCLE ( 'NONE', #8098, 9.000000000000001776 ) ;
#18051=CARTESIAN_POINT ( 'NONE',  ( -0.8801090646609045498, 81.98100004360541959, -99.03135606234927479 ) ) ;
#18077=CONICAL_SURFACE ( 'NONE', #6343, 9.000000000000001776, 1.047197551196594301 ) ;
#18120=CARTESIAN_POINT ( 'NONE',  ( -7.774884586432871281, 81.99999999999997158, -96.16248895089307780 ) ) ;
#18161=PLANE ( 'NONE',  #10947 ) ;
#18164=CARTESIAN_POINT ( 'NONE',  ( 3.866440703273595680, 70.35631045439365039, -81.75340644824426306 ) ) ;
#18185=CARTESIAN_POINT ( 'NONE',  ( 0.8743530591963392107, 81.99999999999995737, -98.80339646031046641 ) ) ;
#18249=CARTESIAN_POINT ( 'NONE',  ( 9.142505149400571796, 81.19615242270661781, -88.65345271381767134 ) ) ;
#18309=PLANE ( 'NONE',  #12916 ) ;
#18327=VERTEX_POINT ( 'NONE', #8142 ) ;
#18331=AXIS2_PLACEMENT_3D ( 'NONE', #19477, #17550, #14463 ) ;
#18365=CARTESIAN_POINT ( 'NONE',  ( -5.156377330703347361, 81.19615242270661781, -99.58697729741749072 ) ) ;
#18374=CARTESIAN_POINT ( 'NONE',  ( -4.315545553080795571, 81.44091995301853615, -99.47772690391978756 ) ) ;
#18386=ORIENTED_EDGE ( 'NONE', *, *, #10434, .T. ) ;
#18391=FACE_OUTER_BOUND ( 'NONE', #8710, .T. ) ;
#18403=VERTEX_POINT ( 'NONE', #21745 ) ;
#18439=CARTESIAN_POINT ( 'NONE',  ( 4.376210989365964643, 81.97459999999998104, -92.29796090835097289 ) ) ;
#18444=CARTESIAN_POINT ( 'NONE',  ( -6.702556532201372264, 69.99999999999998579, -87.68700545388549017 ) ) ;
#18470=AXIS2_PLACEMENT_3D ( 'NONE', #648, #16745, #15017 ) ;
#18519=CARTESIAN_POINT ( 'NONE',  ( -9.809641362382286900, 69.99999999999998579, -87.34492244913440118 ) ) ;
#18577=ADVANCED_FACE ( 'NONE', ( #6387 ), #15354, .F. ) ;
#18590=CARTESIAN_POINT ( 'NONE',  ( -6.702556532201369599, 95.03750572909316929, -87.68700545388549017 ) ) ;
#18604=DIRECTION ( 'NONE',  ( -5.440186201345738641E-18, -1.000000000000000000, -1.334940939666364181E-17 ) ) ;
#18627=EDGE_CURVE ( 'NONE', #20328, #5755, #6758, .T. ) ;
#18694=DIRECTION ( 'NONE',  ( -5.440186201345738641E-18, -1.000000000000000000, -1.334940939666364181E-17 ) ) ;
#18711=B_SPLINE_CURVE_WITH_KNOTS ( 'NONE', 3,
 ( #4140, #9078, #16586, #2546, #18185, #21808 ),
 .UNSPECIFIED., .F., .F.,
 ( 4, 2, 4 ),
 ( 2.380730968155625444E-07, 0.002629065763328323601, 0.005257893453559830781 ),
 .UNSPECIFIED. ) ;
#18726=ADVANCED_FACE ( 'NONE', ( #21572 ), #18077, .T. ) ;
#18730=ORIENTED_EDGE ( 'NONE', *, *, #14262, .F. ) ;
#18759=( NAMED_UNIT ( * ) PLANE_ANGLE_UNIT ( ) SI_UNIT ( $, .RADIAN. ) );
#18776=CARTESIAN_POINT ( 'NONE',  ( -1.163172771417702700, 81.99999999999998579, -89.99248318111824574 ) ) ;
#18781=DIRECTION ( 'NONE',  ( -5.440186201345738641E-18, -1.000000000000000000, -1.334940939666364181E-17 ) ) ;
#18790=DIRECTION ( 'NONE',  ( 5.440186201345738641E-18, 1.000000000000000000, 1.334940939666364181E-17 ) ) ;
#18795=EDGE_LOOP ( 'NONE', ( #5001, #20707, #8135 ) ) ;
#18799=CARTESIAN_POINT ( 'NONE',  ( 7.055447609860087788, 70.09252763182291801, -85.92399523110741200 ) ) ;
#18841=CARTESIAN_POINT ( 'NONE',  ( -9.472248412593195610, 81.99999999999998579, -86.53426659026914081 ) ) ;
#18873=FACE_OUTER_BOUND ( 'NONE', #6731, .T. ) ;
#18903=CARTESIAN_POINT ( 'NONE',  ( 9.142505149400571796, 70.80384757729338219, -88.65345271381767134 ) ) ;
#18907=B_SPLINE_CURVE_WITH_KNOTS ( 'NONE', 3,
 ( #21562, #5837, #18164, #12867, #2417, #16443 ),
 .UNSPECIFIED., .F., .F.,
 ( 4, 2, 4 ),
 ( 2.380730968161660289E-07, 0.002629065763328376944, 0.005257893453559938333 ),
 .UNSPECIFIED. ) ;
#18943=B_SPLINE_CURVE_WITH_KNOTS ( 'NONE', 3,
 ( #19873, #14633, #14868, #12901, #18519, #2779 ),
 .UNSPECIFIED., .F., .F.,
 ( 4, 2, 4 ),
 ( 0.009270618776430233909, 0.01189894710419334839, 0.01452727543195646287 ),
 .UNSPECIFIED. ) ;
#18964=DIRECTION ( 'NONE',  ( -5.440186201345738641E-18, -1.000000000000000000, -1.334940939666364181E-17 ) ) ;
#19049=CARTESIAN_POINT ( 'NONE',  ( 7.145902869757795983, 81.99999999999998579, -93.45069977196735067 ) ) ;
#19149=CARTESIAN_POINT ( 'NONE',  ( 9.142505149400548703, 81.99999999999998579, -88.65345271381772818 ) ) ;
#19190=CIRCLE ( 'NONE', #18470, 5.100000000000004974 ) ;
#19220=VERTEX_POINT ( 'NONE', #18249 ) ;
#19263=CARTESIAN_POINT ( 'NONE',  ( -1.163172771417702700, 81.34441321561124028, -89.99248318111824574 ) ) ;
#19299=ORIENTED_EDGE ( 'NONE', *, *, #5185, .F. ) ;
#19300=CARTESIAN_POINT ( 'NONE',  ( -8.849534454763640312, 81.98100004360546222, -94.75705998267450525 ) ) ;
#19413=ORIENTED_EDGE ( 'NONE', *, *, #7053, .T. ) ;
#19468=CIRCLE ( 'NONE', #11061, 9.000000000000001776 ) ;
#19477=CARTESIAN_POINT ( 'NONE',  ( -17.78132405376864966, 81.99999999999998579, -83.07604999942009272 ) ) ;
#19498=DIRECTION ( 'NONE',  ( 0.9232306267972774094, 0.000000000000000000, -0.3842462878721227826 ) ) ;
#19518=CARTESIAN_POINT ( 'NONE',  ( 4.376210989365964643, 81.99999999999998579, -92.29796090835097289 ) ) ;
#19528=EDGE_CURVE ( 'NONE', #440, #4475, #19190, .T. ) ;
#19557=CARTESIAN_POINT ( 'NONE',  ( -1.163172771417702700, 70.69320546282760631, -89.99248318111824574 ) ) ;
#19584=CARTESIAN_POINT ( 'NONE',  ( -5.156377330703347361, 70.80384757729338219, -99.58697729741749072 ) ) ;
#19593=EDGE_CURVE ( 'NONE', #20328, #10931, #8102, .T. ) ;
#19668=VECTOR ( 'NONE', #8162, 1000.000000000000000 ) ;
#19679=ORIENTED_EDGE ( 'NONE', *, *, #6568, .T. ) ;
#19717=CARTESIAN_POINT ( 'NONE',  ( 5.149300590115022835, 70.80384757729338219, -98.24794683011701579 ) ) ;
#19794=CARTESIAN_POINT ( 'NONE',  ( -4.315545553080798236, 70.55908004698144964, -99.47772690391983019 ) ) ;
#19809=PRODUCT_DEFINITION_FORMATION_WITH_SPECIFIED_SOURCE ( 'ANY', '', #14902, .NOT_KNOWN. ) ;
#19817=FACE_OUTER_BOUND ( 'NONE', #12583, .T. ) ;
#19873=CARTESIAN_POINT ( 'NONE',  ( -11.46885069223597853, 70.80384757729338219, -91.33151364841882014 ) ) ;
#19880=FACE_OUTER_BOUND ( 'NONE', #21973, .T. ) ;
#19898=CARTESIAN_POINT ( 'NONE',  ( 5.149300590115022835, 81.19615242270661781, -98.24794683011701579 ) ) ;
#19913=EDGE_LOOP ( 'NONE', ( #15130, #2176, #22118 ) ) ;
#19933=CARTESIAN_POINT ( 'NONE',  ( -1.163172771417702700, 81.97459999999998104, -89.99248318111824574 ) ) ;
#19957=VERTEX_POINT ( 'NONE', #19898 ) ;
#19967=CARTESIAN_POINT ( 'NONE',  ( 1.141353067861252013, 81.64298031427460955, -80.61740134152157111 ) ) ;
#20031=ADVANCED_FACE ( 'NONE', ( #10145 ), #14480, .T. ) ;
#20081=EDGE_CURVE ( 'NONE', #18403, #2761, #6732, .T. ) ;
#20143=ORIENTED_EDGE ( 'NONE', *, *, #14900, .T. ) ;
#20153=DIRECTION ( 'NONE',  ( -0.9232306267972774094, 0.000000000000000000, 0.3842462878721227826 ) ) ;
#20183=EDGE_LOOP ( 'NONE', ( #15075, #17, #4032 ) ) ;
#20227=ORIENTED_EDGE ( 'NONE', *, *, #1671, .T. ) ;
#20298=B_SPLINE_CURVE_WITH_KNOTS ( 'NONE', 3,
 ( #1354, #11685, #15374, #18799, #3062, #20628, #12133, #18903 ),
 .UNSPECIFIED., .F., .F.,
 ( 4, 2, 2, 4 ),
 ( 0.005257893453559938333, 0.006567392922673252059, 0.007876892391786564918, 0.01049589133001322533 ),
 .UNSPECIFIED. ) ;
#20328=VERTEX_POINT ( 'NONE', #9668 ) ;
#20329=CARTESIAN_POINT ( 'NONE',  ( -1.163172771417702700, 81.99999999999998579, -89.99248318111824574 ) ) ;
#20391=DIRECTION ( 'NONE',  ( 0.9232306267972772984, 0.000000000000000000, -0.3842462878721232822 ) ) ;
#20401=VERTEX_POINT ( 'NONE', #13984 ) ;
#20408=DIRECTION ( 'NONE',  ( -5.440186201345738641E-18, -1.000000000000000000, -1.334940939666364181E-17 ) ) ;
#20417=CONICAL_SURFACE ( 'NONE', #13486, 9.000000000000001776, 1.047197551196594301 ) ;
#20429=CARTESIAN_POINT ( 'NONE',  ( 5.448539043597403264, 81.99999999999998579, -83.82247741134344210 ) ) ;
#20577=CARTESIAN_POINT ( 'NONE',  ( -1.163172771417702700, 81.99999999999998579, -89.99248318111824574 ) ) ;
#20627=ORIENTED_EDGE ( 'NONE', *, *, #1671, .F. ) ;
#20628=CARTESIAN_POINT ( 'NONE',  ( 8.108149183870599686, 70.35701968572533360, -87.30072018181319038 ) ) ;
#20665=CARTESIAN_POINT ( 'NONE',  ( 8.819665691964022614, 81.43869406011346257, -89.42914081817023941 ) ) ;
#20707=ORIENTED_EDGE ( 'NONE', *, *, #12077, .T. ) ;
#20751=SURFACE_SIDE_STYLE ('',( #1585 ) ) ;
#20753=ORIENTED_EDGE ( 'NONE', *, *, #2863, .T. ) ;
#20776=DIRECTION ( 'NONE',  ( 5.440186201345738641E-18, 1.000000000000000000, 1.334940939666364181E-17 ) ) ;
#20861=AXIS2_PLACEMENT_3D ( 'NONE', #22569, #3430, #4912 ) ;
#20872=AXIS2_PLACEMENT_3D ( 'NONE', #16848, #18781, #1232 ) ;
#20894=CARTESIAN_POINT ( 'NONE',  ( -1.163172771417702700, 69.99999999999998579, -89.99248318111824574 ) ) ;
#20909=VERTEX_POINT ( 'NONE', #22210 ) ;
#20965=DIRECTION ( 'NONE',  ( -0.9916643202943333790, 7.114886815082618290E-18, -0.1288482667915160917 ) ) ;
#20991=DIRECTION ( 'NONE',  ( 5.440186201345738641E-18, 1.000000000000000000, 1.334940939666364181E-17 ) ) ;
#21013=CARTESIAN_POINT ( 'NONE',  ( -10.43449472670604550, 70.35701968572537623, -92.68424618042337215 ) ) ;
#21027=CARTESIAN_POINT ( 'NONE',  ( -10.43449472670604372, 81.64298031427460955, -92.68424618042337215 ) ) ;
#21050=AXIS2_PLACEMENT_3D ( 'NONE', #20577, #9806, #8398 ) ;
#21083=ADVANCED_FACE ( 'NONE', ( #9708 ), #18309, .T. ) ;
#21128=DIRECTION ( 'NONE',  ( -5.440186201345738641E-18, -1.000000000000000000, -1.334940939666364181E-17 ) ) ;
#21163=ORIENTED_EDGE ( 'NONE', *, *, #22347, .T. ) ;
#21195=CARTESIAN_POINT ( 'NONE',  ( -7.475646132950445555, 70.80384757729335377, -81.73701953211951832 ) ) ;
#21200=VERTEX_POINT ( 'NONE', #15451 ) ;
#21216=FACE_OUTER_BOUND ( 'NONE', #21312, .T. ) ;
#21259=EDGE_CURVE ( 'NONE', #16597, #3063, #7017, .T. ) ;
#21279=FACE_OUTER_BOUND ( 'NONE', #16824, .T. ) ;
#21292=EDGE_CURVE ( 'NONE', #1068, #12626, #18943, .T. ) ;
#21303=CARTESIAN_POINT ( 'NONE',  ( -6.192786246109094783, 81.64368954560633540, -98.23155991399221421 ) ) ;
#21308=CARTESIAN_POINT ( 'NONE',  ( -8.792471272935648230, 70.07756262466200781, -84.90096239309924897 ) ) ;
#21312=EDGE_LOOP ( 'NONE', ( #13042, #19299, #2235 ) ) ;
#21331=CARTESIAN_POINT ( 'NONE',  ( -11.46885069223597853, 81.19615242270661781, -91.33151364841882014 ) ) ;
#21336=CARTESIAN_POINT ( 'NONE',  ( -1.163172771417702700, 69.99999999999998579, -89.99248318111824574 ) ) ;
#21347=CARTESIAN_POINT ( 'NONE',  ( -1.163172771417702700, 69.99999999999998579, -89.99248318111824574 ) ) ;
#21355=CARTESIAN_POINT ( 'NONE',  ( -11.46885069223597853, 81.19615242270661781, -91.33151364841882014 ) ) ;
#21375=DIRECTION ( 'NONE',  ( 0.9232306267972774094, 0.000000000000000000, -0.3842462878721227826 ) ) ;
#21421=DIRECTION ( 'NONE',  ( -0.9232306267972777425, 0.000000000000000000, 0.3842462878721220054 ) ) ;
#21516=CARTESIAN_POINT ( 'NONE',  ( -2.180642712250698612, 70.14698466122827369, -99.20033613248658355 ) ) ;
#21525=DIRECTION ( 'NONE',  ( 5.440186201345738641E-18, 1.000000000000000000, 1.334940939666364181E-17 ) ) ;
#21543=AXIS2_PLACEMENT_3D ( 'NONE', #20894, #15994, #22590 ) ;
#21562=CARTESIAN_POINT ( 'NONE',  ( 2.830031787867828275, 70.80384757729338219, -80.39798906481894392 ) ) ;
#21572=FACE_OUTER_BOUND ( 'NONE', #4582, .T. ) ;
#21591=CARTESIAN_POINT ( 'NONE',  ( -9.472248412593195610, 81.99999999999998579, -86.53426659026914081 ) ) ;
#21608=FACE_OUTER_BOUND ( 'NONE', #15956, .T. ) ;
#21618=DIRECTION ( 'NONE',  ( 0.9232306267972774094, 0.000000000000000000, -0.3842462878721227826 ) ) ;
#21662=CARTESIAN_POINT ( 'NONE',  ( -11.46885069223597853, 81.19615242270661781, -91.33151364841882014 ) ) ;
#21672=AXIS2_PLACEMENT_3D ( 'NONE', #9741, #11337, #13084 ) ;
#21701=DIRECTION ( 'NONE',  ( 0.9232306267972777425, 0.000000000000000000, -0.3842462878721220054 ) ) ;
#21711=DIRECTION ( 'NONE',  ( 0.9232306267972777425, 0.000000000000000000, -0.3842462878721220054 ) ) ;
#21745=CARTESIAN_POINT ( 'NONE',  ( -0.003538370294055813436, 69.99999999999998579, -98.91746206376724615 ) ) ;
#21749=DIRECTION ( 'NONE',  ( -5.440186201345738641E-18, -1.000000000000000000, -1.334940939666364181E-17 ) ) ;
#21806=VERTEX_POINT ( 'NONE', #1037 ) ;
#21808=CARTESIAN_POINT ( 'NONE',  ( -0.003538370294055813436, 81.99999999999998579, -98.91746206376724615 ) ) ;
#21848=EDGE_LOOP ( 'NONE', ( #9039, #11085, #6165 ) ) ;
#21866=ORIENTED_EDGE ( 'NONE', *, *, #10667, .F. ) ;
#21913=LINE ( 'NONE', #4803, #22545 ) ;
#21938=AXIS2_PLACEMENT_3D ( 'NONE', #17877, #2110, #9221 ) ;
#21939=EDGE_CURVE ( 'NONE', #1692, #680, #22050, .T. ) ;
#21973=EDGE_LOOP ( 'NONE', ( #4661, #13875, #20753, #12991, #17736, #19413 ) ) ;
#22030=CIRCLE ( 'NONE', #4122, 9.000000000000001776 ) ;
#22036=CYLINDRICAL_SURFACE ( 'NONE', #22385, 6.000000000000000888 ) ;
#22050=CIRCLE ( 'NONE', #5938, 6.000000000000004441 ) ;
#22055=ORIENTED_EDGE ( 'NONE', *, *, #15287, .T. ) ;
#22080=DIRECTION ( 'NONE',  ( -0.9232306267972774094, 0.000000000000000000, 0.3842462878721227826 ) ) ;
#22095=CIRCLE ( 'NONE', #12232, 9.000000000000000000 ) ;
#22098=FACE_OUTER_BOUND ( 'NONE', #19913, .T. ) ;
#22099=ORIENTED_EDGE ( 'NONE', *, *, #3112, .T. ) ;
#22111=DIRECTION ( 'NONE',  ( 0.9232306267972768543, 0.000000000000000000, -0.3842462878721243924 ) ) ;
#22117=EDGE_CURVE ( 'NONE', #21200, #12626, #11039, .T. ) ;
#22118=ORIENTED_EDGE ( 'NONE', *, *, #14196, .F. ) ;
#22166=CARTESIAN_POINT ( 'NONE',  ( 5.806620212786450352, 81.64473548815914228, -96.66860143004626593 ) ) ;
#22191=DIRECTION ( 'NONE',  ( 5.440186201345738641E-18, 1.000000000000000000, 1.334940939666364181E-17 ) ) ;
#22208=CARTESIAN_POINT ( 'NONE',  ( 8.108149183870601462, 81.64298031427468061, -87.30072018181317617 ) ) ;
#22210=CARTESIAN_POINT ( 'NONE',  ( -5.156377330703347361, 70.80384757729338219, -99.58697729741749072 ) ) ;
#22250=CARTESIAN_POINT ( 'NONE',  ( -1.163172771417702700, 81.99999999999998579, -89.99248318111824574 ) ) ;
#22346=CARTESIAN_POINT ( 'NONE',  ( -7.774884586432870393, 70.00000000000002842, -96.16248895089307780 ) ) ;
#22347=EDGE_CURVE ( 'NONE', #3063, #19220, #15456, .T. ) ;
#22356=DIRECTION ( 'NONE',  ( 5.440186201345738641E-18, 1.000000000000000000, 1.334940939666364181E-17 ) ) ;
#22385=AXIS2_PLACEMENT_3D ( 'NONE', #4359, #14751, #21701 ) ;
#22395=CARTESIAN_POINT ( 'NONE',  ( 5.149300590115022835, 70.80384757729338219, -98.24794683011701579 ) ) ;
#22406=AXIS2_PLACEMENT_3D ( 'NONE', #19557, #9088, #268 ) ;
#22445=CARTESIAN_POINT ( 'NONE',  ( -7.475646132950445555, 70.80384757729335377, -81.73701953211951832 ) ) ;
#22475=ORIENTED_EDGE ( 'NONE', *, *, #12077, .F. ) ;
#22541=DIRECTION ( 'NONE',  ( 0.6074180324222079319, 7.300068142772960434E-18, -0.7943823600057678957 ) ) ;
#22545=VECTOR ( 'NONE', #6092, 999.9999999999998863 ) ;
#22548=ADVANCED_FACE ( 'NONE', ( #16908 ), #22036, .F. ) ;
#22569=CARTESIAN_POINT ( 'NONE',  ( -1.163172771417702700, 69.99999999999998579, -89.99248318111824574 ) ) ;
#22570=CARTESIAN_POINT ( 'NONE',  ( -1.163172771417702700, 81.97459999999998104, -89.99248318111824574 ) ) ;
#22582=ORIENTED_EDGE ( 'NONE', *, *, #10191, .T. ) ;
#22590=DIRECTION ( 'NONE',  ( 0.9232306267972777425, 0.000000000000000000, -0.3842462878721221164 ) ) ;
#22641=ORIENTED_EDGE ( 'NONE', *, *, #17372, .F. ) ;
#22647=AXIS2_PLACEMENT_3D ( 'NONE', #13065, #14668, #4520 ) ;
ENDSEC;
END-ISO-10303-21;
